ISO-10303-21;
HEADER;
/* Generated by software containing ST-Developer
 * from STEP Tools, Inc. (www.steptools.com) 
 */

FILE_DESCRIPTION(
/* description */ (''),
/* implementation_level */ '2;1');

FILE_NAME(
/* name */ 'Middle_Ring.step',
/* time_stamp */ '2026-10-23T17:22:31+06:00',
/* author */ (''),
/* organization */ (''),
/* preprocessor_version */ 'ST-DEVELOPER v20.2',
/* originating_system */ 'Autodesk Translation Framework v15.15.0.0',
/* authorisation */ '');

FILE_SCHEMA (('AUTOMOTIVE_DESIGN { 1 0 10303 214 3 1 1 }'));
ENDSEC;

DATA;
#10=MECHANICAL_DESIGN_GEOMETRIC_PRESENTATION_REPRESENTATION('',(#80),#7315);
#60=SHAPE_REPRESENTATION_RELATIONSHIP('SRR','None',#7356,#70);
#70=ADVANCED_BREP_SHAPE_REPRESENTATION('',(#90),#7308);
#80=STYLED_ITEM('',(#7431),#90);
#90=MANIFOLD_SOLID_BREP('Middle_Ring',#3217);
#101=CONICAL_SURFACE('',#3552,10.265215394118,0.787617500807741);
#102=CONICAL_SURFACE('',#3635,10.265215394118,0.783178825987157);
#168=B_SPLINE_CURVE_WITH_KNOTS('',3,(#6051,#6052,#6053,#6054,#6055,#6056,
#6057,#6058,#6059,#6060,#6061,#6062,#6063,#6064),.UNSPECIFIED.,.F.,.F.,
(4,2,2,2,2,2,4),(0.0804140797636754,0.103753655307869,0.138766322922265,
0.173778990536662,0.208791658151058,0.243804325765454,0.267143901309648),
 .UNSPECIFIED.);
#169=B_SPLINE_CURVE_WITH_KNOTS('',3,(#6068,#6069,#6070,#6071,#6072,#6073,
#6074,#6075,#6076,#6077,#6078,#6079,#6080,#6081),.UNSPECIFIED.,.F.,.F.,
(4,2,2,2,2,2,4),(0.466102891398403,0.489272506433,0.524287150622646,0.559301794812291,
0.594316439001936,0.629331083191581,0.652500698226179),.UNSPECIFIED.);
#170=B_SPLINE_CURVE_WITH_KNOTS('',3,(#6086,#6087,#6088,#6089,#6090,#6091,
#6092,#6093,#6094,#6095,#6096,#6097,#6098,#6099),.UNSPECIFIED.,.F.,.F.,
(4,2,2,2,2,2,4),(0.0804140797636753,0.103753655307869,0.138766322922265,
0.173778990536662,0.208791658151058,0.243804325765454,0.267143901309648),
 .UNSPECIFIED.);
#171=B_SPLINE_CURVE_WITH_KNOTS('',3,(#6103,#6104,#6105,#6106,#6107,#6108,
#6109,#6110,#6111,#6112,#6113,#6114,#6115,#6116),.UNSPECIFIED.,.F.,.F.,
(4,2,2,2,2,2,4),(0.466102891398403,0.489272506433,0.524287150622645,0.55930179481229,
0.594316439001936,0.629331083191581,0.652500698226178),.UNSPECIFIED.);
#172=B_SPLINE_CURVE_WITH_KNOTS('',3,(#6121,#6122,#6123,#6124,#6125,#6126,
#6127,#6128,#6129,#6130,#6131,#6132,#6133,#6134),.UNSPECIFIED.,.F.,.F.,
(4,2,2,2,2,2,4),(0.0804140797636755,0.103753655307869,0.138766322922265,
0.173778990536661,0.208791658151058,0.243804325765454,0.267143901309647),
 .UNSPECIFIED.);
#173=B_SPLINE_CURVE_WITH_KNOTS('',3,(#6138,#6139,#6140,#6141,#6142,#6143,
#6144,#6145,#6146,#6147,#6148,#6149,#6150,#6151),.UNSPECIFIED.,.F.,.F.,
(4,2,2,2,2,2,4),(0.466102891398403,0.489272506433,0.524287150622646,0.559301794812291,
0.594316439001936,0.629331083191582,0.652500698226179),.UNSPECIFIED.);
#174=B_SPLINE_CURVE_WITH_KNOTS('',3,(#6156,#6157,#6158,#6159,#6160,#6161,
#6162,#6163,#6164,#6165,#6166,#6167,#6168,#6169),.UNSPECIFIED.,.F.,.F.,
(4,2,2,2,2,2,4),(0.0804140797636754,0.103753655307869,0.138766322922265,
0.173778990536662,0.208791658151058,0.243804325765454,0.267143901309648),
 .UNSPECIFIED.);
#175=B_SPLINE_CURVE_WITH_KNOTS('',3,(#6173,#6174,#6175,#6176,#6177,#6178,
#6179,#6180,#6181,#6182,#6183,#6184,#6185,#6186),.UNSPECIFIED.,.F.,.F.,
(4,2,2,2,2,2,4),(0.466102891398402,0.489272506433,0.524287150622646,0.559301794812291,
0.594316439001936,0.629331083191581,0.652500698226179),.UNSPECIFIED.);
#176=B_SPLINE_CURVE_WITH_KNOTS('',3,(#6191,#6192,#6193,#6194,#6195,#6196,
#6197,#6198,#6199,#6200,#6201,#6202,#6203,#6204),.UNSPECIFIED.,.F.,.F.,
(4,2,2,2,2,2,4),(0.0804140797636755,0.103753655307869,0.138766322922265,
0.173778990536661,0.208791658151058,0.243804325765454,0.267143901309648),
 .UNSPECIFIED.);
#177=B_SPLINE_CURVE_WITH_KNOTS('',3,(#6208,#6209,#6210,#6211,#6212,#6213,
#6214,#6215,#6216,#6217,#6218,#6219,#6220,#6221),.UNSPECIFIED.,.F.,.F.,
(4,2,2,2,2,2,4),(0.466102891398402,0.489272506433,0.524287150622645,0.55930179481229,
0.594316439001935,0.629331083191581,0.652500698226178),.UNSPECIFIED.);
#178=B_SPLINE_CURVE_WITH_KNOTS('',3,(#6226,#6227,#6228,#6229,#6230,#6231,
#6232,#6233,#6234,#6235,#6236,#6237,#6238,#6239),.UNSPECIFIED.,.F.,.F.,
(4,2,2,2,2,2,4),(0.0804140797636754,0.103753655307869,0.138766322922265,
0.173778990536662,0.208791658151058,0.243804325765454,0.267143901309648),
 .UNSPECIFIED.);
#179=B_SPLINE_CURVE_WITH_KNOTS('',3,(#6243,#6244,#6245,#6246,#6247,#6248,
#6249,#6250,#6251,#6252,#6253,#6254,#6255,#6256),.UNSPECIFIED.,.F.,.F.,
(4,2,2,2,2,2,4),(0.466102891398402,0.489272506433,0.524287150622645,0.559301794812291,
0.594316439001936,0.629331083191581,0.652500698226179),.UNSPECIFIED.);
#180=B_SPLINE_CURVE_WITH_KNOTS('',3,(#6261,#6262,#6263,#6264,#6265,#6266,
#6267,#6268,#6269,#6270,#6271,#6272,#6273,#6274),.UNSPECIFIED.,.F.,.F.,
(4,2,2,2,2,2,4),(0.0804140797636753,0.103753655307869,0.138766322922265,
0.173778990536662,0.208791658151058,0.243804325765455,0.267143901309648),
 .UNSPECIFIED.);
#181=B_SPLINE_CURVE_WITH_KNOTS('',3,(#6278,#6279,#6280,#6281,#6282,#6283,
#6284,#6285,#6286,#6287,#6288,#6289,#6290,#6291),.UNSPECIFIED.,.F.,.F.,
(4,2,2,2,2,2,4),(0.466102891398403,0.489272506433,0.524287150622645,0.559301794812291,
0.594316439001936,0.629331083191581,0.652500698226179),.UNSPECIFIED.);
#182=B_SPLINE_CURVE_WITH_KNOTS('',3,(#6296,#6297,#6298,#6299,#6300,#6301,
#6302,#6303,#6304,#6305,#6306,#6307,#6308,#6309),.UNSPECIFIED.,.F.,.F.,
(4,2,2,2,2,2,4),(0.0804140797636755,0.103753655307869,0.138766322922265,
0.173778990536662,0.208791658151058,0.243804325765455,0.267143901309648),
 .UNSPECIFIED.);
#183=B_SPLINE_CURVE_WITH_KNOTS('',3,(#6313,#6314,#6315,#6316,#6317,#6318,
#6319,#6320,#6321,#6322,#6323,#6324,#6325,#6326),.UNSPECIFIED.,.F.,.F.,
(4,2,2,2,2,2,4),(0.466102891398403,0.489272506433,0.524287150622645,0.55930179481229,
0.594316439001936,0.629331083191581,0.652500698226179),.UNSPECIFIED.);
#184=B_SPLINE_CURVE_WITH_KNOTS('',3,(#6331,#6332,#6333,#6334,#6335,#6336,
#6337,#6338,#6339,#6340,#6341,#6342,#6343,#6344),.UNSPECIFIED.,.F.,.F.,
(4,2,2,2,2,2,4),(0.0804140797636754,0.103753655307869,0.138766322922265,
0.173778990536661,0.208791658151058,0.243804325765454,0.267143901309648),
 .UNSPECIFIED.);
#185=B_SPLINE_CURVE_WITH_KNOTS('',3,(#6348,#6349,#6350,#6351,#6352,#6353,
#6354,#6355,#6356,#6357,#6358,#6359,#6360,#6361),.UNSPECIFIED.,.F.,.F.,
(4,2,2,2,2,2,4),(0.466102891398402,0.489272506433,0.524287150622645,0.55930179481229,
0.594316439001936,0.629331083191581,0.652500698226179),.UNSPECIFIED.);
#186=B_SPLINE_CURVE_WITH_KNOTS('',3,(#6366,#6367,#6368,#6369,#6370,#6371,
#6372,#6373,#6374,#6375,#6376,#6377,#6378,#6379),.UNSPECIFIED.,.F.,.F.,
(4,2,2,2,2,2,4),(0.0804140797636754,0.103753655307869,0.138766322922265,
0.173778990536662,0.208791658151058,0.243804325765454,0.267143901309648),
 .UNSPECIFIED.);
#187=B_SPLINE_CURVE_WITH_KNOTS('',3,(#6383,#6384,#6385,#6386,#6387,#6388,
#6389,#6390,#6391,#6392,#6393,#6394,#6395,#6396),.UNSPECIFIED.,.F.,.F.,
(4,2,2,2,2,2,4),(0.466102891398402,0.489272506433,0.524287150622645,0.55930179481229,
0.594316439001935,0.62933108319158,0.652500698226178),.UNSPECIFIED.);
#188=B_SPLINE_CURVE_WITH_KNOTS('',3,(#6401,#6402,#6403,#6404,#6405,#6406,
#6407,#6408,#6409,#6410,#6411,#6412,#6413,#6414),.UNSPECIFIED.,.F.,.F.,
(4,2,2,2,2,2,4),(0.0804140797636753,0.103753655307869,0.138766322922265,
0.173778990536661,0.208791658151058,0.243804325765454,0.267143901309648),
 .UNSPECIFIED.);
#189=B_SPLINE_CURVE_WITH_KNOTS('',3,(#6418,#6419,#6420,#6421,#6422,#6423,
#6424,#6425,#6426,#6427,#6428,#6429,#6430,#6431),.UNSPECIFIED.,.F.,.F.,
(4,2,2,2,2,2,4),(0.466102891398402,0.489272506432999,0.524287150622645,
0.55930179481229,0.594316439001935,0.62933108319158,0.652500698226178),
 .UNSPECIFIED.);
#190=B_SPLINE_CURVE_WITH_KNOTS('',3,(#6436,#6437,#6438,#6439,#6440,#6441,
#6442,#6443,#6444,#6445,#6446,#6447,#6448,#6449),.UNSPECIFIED.,.F.,.F.,
(4,2,2,2,2,2,4),(0.0804140797636754,0.103753655307869,0.138766322922265,
0.173778990536661,0.208791658151058,0.243804325765454,0.267143901309648),
 .UNSPECIFIED.);
#191=B_SPLINE_CURVE_WITH_KNOTS('',3,(#6453,#6454,#6455,#6456,#6457,#6458,
#6459,#6460,#6461,#6462,#6463,#6464,#6465,#6466),.UNSPECIFIED.,.F.,.F.,
(4,2,2,2,2,2,4),(0.466102891398402,0.489272506433,0.524287150622645,0.55930179481229,
0.594316439001935,0.629331083191581,0.652500698226178),.UNSPECIFIED.);
#192=B_SPLINE_CURVE_WITH_KNOTS('',3,(#6471,#6472,#6473,#6474,#6475,#6476,
#6477,#6478,#6479,#6480,#6481,#6482,#6483,#6484),.UNSPECIFIED.,.F.,.F.,
(4,2,2,2,2,2,4),(0.0804140797636754,0.103753655307869,0.138766322922265,
0.173778990536662,0.208791658151058,0.243804325765454,0.267143901309648),
 .UNSPECIFIED.);
#193=B_SPLINE_CURVE_WITH_KNOTS('',3,(#6488,#6489,#6490,#6491,#6492,#6493,
#6494,#6495,#6496,#6497,#6498,#6499,#6500,#6501),.UNSPECIFIED.,.F.,.F.,
(4,2,2,2,2,2,4),(0.466102891398403,0.489272506433,0.524287150622646,0.559301794812291,
0.594316439001936,0.629331083191581,0.652500698226179),.UNSPECIFIED.);
#194=B_SPLINE_CURVE_WITH_KNOTS('',3,(#6506,#6507,#6508,#6509,#6510,#6511,
#6512,#6513,#6514,#6515,#6516,#6517,#6518,#6519),.UNSPECIFIED.,.F.,.F.,
(4,2,2,2,2,2,4),(0.0804140797636752,0.103753655307869,0.138766322922265,
0.173778990536661,0.208791658151058,0.243804325765454,0.267143901309648),
 .UNSPECIFIED.);
#195=B_SPLINE_CURVE_WITH_KNOTS('',3,(#6523,#6524,#6525,#6526,#6527,#6528,
#6529,#6530,#6531,#6532,#6533,#6534,#6535,#6536),.UNSPECIFIED.,.F.,.F.,
(4,2,2,2,2,2,4),(0.466102891398402,0.489272506432999,0.524287150622644,
0.559301794812289,0.594316439001935,0.62933108319158,0.652500698226178),
 .UNSPECIFIED.);
#196=B_SPLINE_CURVE_WITH_KNOTS('',3,(#6541,#6542,#6543,#6544,#6545,#6546,
#6547,#6548,#6549,#6550,#6551,#6552,#6553,#6554),.UNSPECIFIED.,.F.,.F.,
(4,2,2,2,2,2,4),(0.0804140797636753,0.103753655307869,0.138766322922265,
0.173778990536662,0.208791658151058,0.243804325765455,0.267143901309648),
 .UNSPECIFIED.);
#197=B_SPLINE_CURVE_WITH_KNOTS('',3,(#6558,#6559,#6560,#6561,#6562,#6563,
#6564,#6565,#6566,#6567,#6568,#6569,#6570,#6571),.UNSPECIFIED.,.F.,.F.,
(4,2,2,2,2,2,4),(0.466102891398402,0.489272506432999,0.524287150622644,
0.55930179481229,0.594316439001935,0.62933108319158,0.652500698226178),
 .UNSPECIFIED.);
#198=B_SPLINE_CURVE_WITH_KNOTS('',3,(#6576,#6577,#6578,#6579,#6580,#6581,
#6582,#6583,#6584,#6585,#6586,#6587,#6588,#6589),.UNSPECIFIED.,.F.,.F.,
(4,2,2,2,2,2,4),(0.0804140797636755,0.103753655307869,0.138766322922265,
0.173778990536661,0.208791658151058,0.243804325765454,0.267143901309648),
 .UNSPECIFIED.);
#199=B_SPLINE_CURVE_WITH_KNOTS('',3,(#6593,#6594,#6595,#6596,#6597,#6598,
#6599,#6600,#6601,#6602,#6603,#6604,#6605,#6606),.UNSPECIFIED.,.F.,.F.,
(4,2,2,2,2,2,4),(0.466102891398403,0.489272506433,0.524287150622646,0.559301794812291,
0.594316439001936,0.629331083191581,0.652500698226179),.UNSPECIFIED.);
#200=B_SPLINE_CURVE_WITH_KNOTS('',3,(#6611,#6612,#6613,#6614,#6615,#6616,
#6617,#6618,#6619,#6620,#6621,#6622,#6623,#6624),.UNSPECIFIED.,.F.,.F.,
(4,2,2,2,2,2,4),(0.0804140797636754,0.103753655307869,0.138766322922265,
0.173778990536662,0.208791658151058,0.243804325765454,0.267143901309648),
 .UNSPECIFIED.);
#201=B_SPLINE_CURVE_WITH_KNOTS('',3,(#6628,#6629,#6630,#6631,#6632,#6633,
#6634,#6635,#6636,#6637,#6638,#6639,#6640,#6641),.UNSPECIFIED.,.F.,.F.,
(4,2,2,2,2,2,4),(0.466102891398403,0.489272506433,0.524287150622646,0.559301794812291,
0.594316439001936,0.629331083191581,0.652500698226179),.UNSPECIFIED.);
#202=B_SPLINE_CURVE_WITH_KNOTS('',3,(#6646,#6647,#6648,#6649,#6650,#6651,
#6652,#6653,#6654,#6655,#6656,#6657,#6658,#6659),.UNSPECIFIED.,.F.,.F.,
(4,2,2,2,2,2,4),(0.0804140797636755,0.103753655307869,0.138766322922265,
0.173778990536662,0.208791658151058,0.243804325765454,0.267143901309648),
 .UNSPECIFIED.);
#203=B_SPLINE_CURVE_WITH_KNOTS('',3,(#6663,#6664,#6665,#6666,#6667,#6668,
#6669,#6670,#6671,#6672,#6673,#6674,#6675,#6676),.UNSPECIFIED.,.F.,.F.,
(4,2,2,2,2,2,4),(0.466102891398403,0.489272506433,0.524287150622645,0.55930179481229,
0.594316439001935,0.62933108319158,0.652500698226178),.UNSPECIFIED.);
#204=B_SPLINE_CURVE_WITH_KNOTS('',3,(#6681,#6682,#6683,#6684,#6685,#6686,
#6687,#6688,#6689,#6690,#6691,#6692,#6693,#6694),.UNSPECIFIED.,.F.,.F.,
(4,2,2,2,2,2,4),(0.0804140797636754,0.103753655307869,0.138766322922265,
0.173778990536662,0.208791658151058,0.243804325765455,0.267143901309648),
 .UNSPECIFIED.);
#205=B_SPLINE_CURVE_WITH_KNOTS('',3,(#6698,#6699,#6700,#6701,#6702,#6703,
#6704,#6705,#6706,#6707,#6708,#6709,#6710,#6711),.UNSPECIFIED.,.F.,.F.,
(4,2,2,2,2,2,4),(0.466102891398403,0.489272506433001,0.524287150622646,
0.559301794812291,0.594316439001936,0.629331083191582,0.65250069822618),
 .UNSPECIFIED.);
#206=B_SPLINE_CURVE_WITH_KNOTS('',3,(#6716,#6717,#6718,#6719,#6720,#6721,
#6722,#6723,#6724,#6725,#6726,#6727,#6728,#6729),.UNSPECIFIED.,.F.,.F.,
(4,2,2,2,2,2,4),(0.0804140797636755,0.103753655307869,0.138766322922265,
0.173778990536661,0.208791658151058,0.243804325765455,0.267143901309648),
 .UNSPECIFIED.);
#207=B_SPLINE_CURVE_WITH_KNOTS('',3,(#6733,#6734,#6735,#6736,#6737,#6738,
#6739,#6740,#6741,#6742,#6743,#6744,#6745,#6746),.UNSPECIFIED.,.F.,.F.,
(4,2,2,2,2,2,4),(0.466102891398403,0.489272506433,0.524287150622645,0.559301794812291,
0.594316439001936,0.629331083191581,0.652500698226178),.UNSPECIFIED.);
#208=B_SPLINE_CURVE_WITH_KNOTS('',3,(#6751,#6752,#6753,#6754,#6755,#6756,
#6757,#6758,#6759,#6760,#6761,#6762,#6763,#6764),.UNSPECIFIED.,.F.,.F.,
(4,2,2,2,2,2,4),(0.0804140797636753,0.103753655307869,0.138766322922265,
0.173778990536662,0.208791658151058,0.243804325765455,0.267143901309648),
 .UNSPECIFIED.);
#209=B_SPLINE_CURVE_WITH_KNOTS('',3,(#6768,#6769,#6770,#6771,#6772,#6773,
#6774,#6775,#6776,#6777,#6778,#6779,#6780,#6781),.UNSPECIFIED.,.F.,.F.,
(4,2,2,2,2,2,4),(0.466102891398403,0.489272506433,0.524287150622646,0.559301794812291,
0.594316439001936,0.629331083191581,0.652500698226179),.UNSPECIFIED.);
#210=B_SPLINE_CURVE_WITH_KNOTS('',3,(#6786,#6787,#6788,#6789,#6790,#6791,
#6792,#6793,#6794,#6795,#6796,#6797,#6798,#6799),.UNSPECIFIED.,.F.,.F.,
(4,2,2,2,2,2,4),(0.0804140797636753,0.103753655307869,0.138766322922265,
0.173778990536662,0.208791658151058,0.243804325765455,0.267143901309648),
 .UNSPECIFIED.);
#211=B_SPLINE_CURVE_WITH_KNOTS('',3,(#6803,#6804,#6805,#6806,#6807,#6808,
#6809,#6810,#6811,#6812,#6813,#6814,#6815,#6816),.UNSPECIFIED.,.F.,.F.,
(4,2,2,2,2,2,4),(0.466102891398403,0.489272506433,0.524287150622646,0.559301794812291,
0.594316439001936,0.629331083191581,0.652500698226179),.UNSPECIFIED.);
#212=B_SPLINE_CURVE_WITH_KNOTS('',3,(#6821,#6822,#6823,#6824,#6825,#6826,
#6827,#6828,#6829,#6830,#6831,#6832,#6833,#6834),.UNSPECIFIED.,.F.,.F.,
(4,2,2,2,2,2,4),(0.0804140797636755,0.103753655307869,0.138766322922265,
0.173778990536661,0.208791658151058,0.243804325765454,0.267143901309648),
 .UNSPECIFIED.);
#213=B_SPLINE_CURVE_WITH_KNOTS('',3,(#6838,#6839,#6840,#6841,#6842,#6843,
#6844,#6845,#6846,#6847,#6848,#6849,#6850,#6851),.UNSPECIFIED.,.F.,.F.,
(4,2,2,2,2,2,4),(0.466102891398403,0.489272506433,0.524287150622646,0.559301794812291,
0.594316439001936,0.629331083191581,0.652500698226179),.UNSPECIFIED.);
#214=B_SPLINE_CURVE_WITH_KNOTS('',3,(#6856,#6857,#6858,#6859,#6860,#6861,
#6862,#6863,#6864,#6865,#6866,#6867,#6868,#6869),.UNSPECIFIED.,.F.,.F.,
(4,2,2,2,2,2,4),(0.0804140797636756,0.103753655307869,0.138766322922265,
0.173778990536662,0.208791658151058,0.243804325765454,0.267143901309648),
 .UNSPECIFIED.);
#215=B_SPLINE_CURVE_WITH_KNOTS('',3,(#6873,#6874,#6875,#6876,#6877,#6878,
#6879,#6880,#6881,#6882,#6883,#6884,#6885,#6886),.UNSPECIFIED.,.F.,.F.,
(4,2,2,2,2,2,4),(0.466102891398403,0.489272506433,0.524287150622645,0.55930179481229,
0.594316439001936,0.629331083191581,0.652500698226178),.UNSPECIFIED.);
#216=B_SPLINE_CURVE_WITH_KNOTS('',3,(#6894,#6895,#6896,#6897,#6898,#6899,
#6900,#6901),.UNSPECIFIED.,.F.,.F.,(4,2,2,4),(0.559301794812291,0.594316439001936,
0.629331083191581,0.652500698226179),.UNSPECIFIED.);
#217=B_SPLINE_CURVE_WITH_KNOTS('',3,(#6928,#6929,#6930,#6931,#6932,#6933,
#6934,#6935),.UNSPECIFIED.,.F.,.F.,(4,2,2,4),(0.466102891398403,0.489272506433001,
0.524287150622646,0.559301794812291),.UNSPECIFIED.);
#218=B_SPLINE_CURVE_WITH_KNOTS('',3,(#6990,#6991,#6992,#6993,#6994,#6995,
#6996,#6997),.UNSPECIFIED.,.F.,.F.,(4,2,2,4),(0.0804140797636754,0.103753655307869,
0.138766322922265,0.173778990536661),.UNSPECIFIED.);
#219=B_SPLINE_CURVE_WITH_KNOTS('',3,(#6998,#6999,#7000,#7001,#7002,#7003,
#7004,#7005),.UNSPECIFIED.,.F.,.F.,(4,2,2,4),(0.173778990536661,0.208791658151058,
0.243804325765454,0.267143901309647),.UNSPECIFIED.);
#312=LINE('',#6066,#472);
#313=LINE('',#6082,#473);
#314=LINE('',#6101,#474);
#315=LINE('',#6117,#475);
#316=LINE('',#6136,#476);
#317=LINE('',#6152,#477);
#318=LINE('',#6171,#478);
#319=LINE('',#6187,#479);
#320=LINE('',#6206,#480);
#321=LINE('',#6222,#481);
#322=LINE('',#6241,#482);
#323=LINE('',#6257,#483);
#324=LINE('',#6276,#484);
#325=LINE('',#6292,#485);
#326=LINE('',#6311,#486);
#327=LINE('',#6327,#487);
#328=LINE('',#6346,#488);
#329=LINE('',#6362,#489);
#330=LINE('',#6381,#490);
#331=LINE('',#6397,#491);
#332=LINE('',#6416,#492);
#333=LINE('',#6432,#493);
#334=LINE('',#6451,#494);
#335=LINE('',#6467,#495);
#336=LINE('',#6486,#496);
#337=LINE('',#6502,#497);
#338=LINE('',#6521,#498);
#339=LINE('',#6537,#499);
#340=LINE('',#6556,#500);
#341=LINE('',#6572,#501);
#342=LINE('',#6591,#502);
#343=LINE('',#6607,#503);
#344=LINE('',#6626,#504);
#345=LINE('',#6642,#505);
#346=LINE('',#6661,#506);
#347=LINE('',#6677,#507);
#348=LINE('',#6696,#508);
#349=LINE('',#6712,#509);
#350=LINE('',#6731,#510);
#351=LINE('',#6747,#511);
#352=LINE('',#6766,#512);
#353=LINE('',#6782,#513);
#354=LINE('',#6801,#514);
#355=LINE('',#6817,#515);
#356=LINE('',#6836,#516);
#357=LINE('',#6852,#517);
#358=LINE('',#6871,#518);
#359=LINE('',#6887,#519);
#360=LINE('',#6892,#520);
#361=LINE('',#6939,#521);
#362=LINE('',#6942,#522);
#363=LINE('',#7009,#523);
#364=LINE('',#7017,#524);
#365=LINE('',#7020,#525);
#472=VECTOR('',#4195,10.);
#473=VECTOR('',#4196,10.);
#474=VECTOR('',#4199,10.);
#475=VECTOR('',#4200,10.);
#476=VECTOR('',#4203,10.);
#477=VECTOR('',#4204,10.);
#478=VECTOR('',#4207,10.);
#479=VECTOR('',#4208,10.);
#480=VECTOR('',#4211,10.);
#481=VECTOR('',#4212,10.);
#482=VECTOR('',#4215,10.);
#483=VECTOR('',#4216,10.);
#484=VECTOR('',#4219,10.);
#485=VECTOR('',#4220,10.);
#486=VECTOR('',#4223,10.);
#487=VECTOR('',#4224,10.);
#488=VECTOR('',#4227,10.);
#489=VECTOR('',#4228,10.);
#490=VECTOR('',#4231,10.);
#491=VECTOR('',#4232,10.);
#492=VECTOR('',#4235,10.);
#493=VECTOR('',#4236,10.);
#494=VECTOR('',#4239,10.);
#495=VECTOR('',#4240,10.);
#496=VECTOR('',#4243,10.);
#497=VECTOR('',#4244,10.);
#498=VECTOR('',#4247,10.);
#499=VECTOR('',#4248,10.);
#500=VECTOR('',#4251,10.);
#501=VECTOR('',#4252,10.);
#502=VECTOR('',#4255,10.);
#503=VECTOR('',#4256,10.);
#504=VECTOR('',#4259,10.);
#505=VECTOR('',#4260,10.);
#506=VECTOR('',#4263,10.);
#507=VECTOR('',#4264,10.);
#508=VECTOR('',#4267,10.);
#509=VECTOR('',#4268,10.);
#510=VECTOR('',#4271,10.);
#511=VECTOR('',#4272,10.);
#512=VECTOR('',#4275,10.);
#513=VECTOR('',#4276,10.);
#514=VECTOR('',#4279,10.);
#515=VECTOR('',#4280,10.);
#516=VECTOR('',#4283,10.);
#517=VECTOR('',#4284,10.);
#518=VECTOR('',#4287,10.);
#519=VECTOR('',#4288,10.);
#520=VECTOR('',#4293,10.265215394118);
#521=VECTOR('',#4348,10.);
#522=VECTOR('',#4351,10.);
#523=VECTOR('',#4448,9.50579594738959);
#524=VECTOR('',#4459,9.50579594738959);
#525=VECTOR('',#4464,10.265215394118);
#624=CYLINDRICAL_SURFACE('',#3528,0.999999999999999);
#625=CYLINDRICAL_SURFACE('',#3529,0.999999999999999);
#626=CYLINDRICAL_SURFACE('',#3530,0.999999999999999);
#627=CYLINDRICAL_SURFACE('',#3531,0.999999999999999);
#628=CYLINDRICAL_SURFACE('',#3532,0.999999999999999);
#629=CYLINDRICAL_SURFACE('',#3533,0.999999999999999);
#630=CYLINDRICAL_SURFACE('',#3534,0.999999999999999);
#631=CYLINDRICAL_SURFACE('',#3535,0.999999999999999);
#632=CYLINDRICAL_SURFACE('',#3536,0.999999999999999);
#633=CYLINDRICAL_SURFACE('',#3537,0.999999999999999);
#634=CYLINDRICAL_SURFACE('',#3538,0.999999999999999);
#635=CYLINDRICAL_SURFACE('',#3539,0.999999999999999);
#636=CYLINDRICAL_SURFACE('',#3540,0.999999999999999);
#637=CYLINDRICAL_SURFACE('',#3541,0.999999999999999);
#638=CYLINDRICAL_SURFACE('',#3542,0.999999999999999);
#639=CYLINDRICAL_SURFACE('',#3543,0.999999999999999);
#640=CYLINDRICAL_SURFACE('',#3544,0.999999999999999);
#641=CYLINDRICAL_SURFACE('',#3545,0.999999999999999);
#642=CYLINDRICAL_SURFACE('',#3546,0.999999999999999);
#643=CYLINDRICAL_SURFACE('',#3547,0.999999999999999);
#644=CYLINDRICAL_SURFACE('',#3548,0.999999999999999);
#645=CYLINDRICAL_SURFACE('',#3549,0.999999999999999);
#646=CYLINDRICAL_SURFACE('',#3550,0.999999999999999);
#647=CYLINDRICAL_SURFACE('',#3551,0.999999999999999);
#648=CYLINDRICAL_SURFACE('',#3579,11.0246348408465);
#649=CYLINDRICAL_SURFACE('',#3581,11.0246348408465);
#650=CYLINDRICAL_SURFACE('',#3583,11.0246348408465);
#651=CYLINDRICAL_SURFACE('',#3585,11.0246348408465);
#652=CYLINDRICAL_SURFACE('',#3587,11.0246348408465);
#653=CYLINDRICAL_SURFACE('',#3589,11.0246348408465);
#654=CYLINDRICAL_SURFACE('',#3591,11.0246348408465);
#655=CYLINDRICAL_SURFACE('',#3593,11.0246348408465);
#656=CYLINDRICAL_SURFACE('',#3595,11.0246348408465);
#657=CYLINDRICAL_SURFACE('',#3597,11.0246348408465);
#658=CYLINDRICAL_SURFACE('',#3599,11.0246348408465);
#659=CYLINDRICAL_SURFACE('',#3601,11.0246348408465);
#660=CYLINDRICAL_SURFACE('',#3603,11.0246348408465);
#661=CYLINDRICAL_SURFACE('',#3605,11.0246348408465);
#662=CYLINDRICAL_SURFACE('',#3607,11.0246348408465);
#663=CYLINDRICAL_SURFACE('',#3609,11.0246348408465);
#664=CYLINDRICAL_SURFACE('',#3611,11.0246348408465);
#665=CYLINDRICAL_SURFACE('',#3613,11.0246348408465);
#666=CYLINDRICAL_SURFACE('',#3615,11.0246348408465);
#667=CYLINDRICAL_SURFACE('',#3617,11.0246348408465);
#668=CYLINDRICAL_SURFACE('',#3619,11.0246348408465);
#669=CYLINDRICAL_SURFACE('',#3621,11.0246348408465);
#670=CYLINDRICAL_SURFACE('',#3623,11.0246348408465);
#671=CYLINDRICAL_SURFACE('',#3625,11.0246348408465);
#672=CYLINDRICAL_SURFACE('',#3627,0.999999999999999);
#673=CYLINDRICAL_SURFACE('',#3628,9.50579594738959);
#674=CYLINDRICAL_SURFACE('',#3633,9.50579594738959);
#675=CYLINDRICAL_SURFACE('',#3637,11.0246348408465);
#710=PLANE('',#3630);
#711=PLANE('',#3631);
#819=FACE_OUTER_BOUND('',#1003,.T.);
#820=FACE_OUTER_BOUND('',#1004,.T.);
#821=FACE_OUTER_BOUND('',#1005,.T.);
#822=FACE_OUTER_BOUND('',#1006,.T.);
#823=FACE_OUTER_BOUND('',#1007,.T.);
#824=FACE_OUTER_BOUND('',#1008,.T.);
#825=FACE_OUTER_BOUND('',#1009,.T.);
#826=FACE_OUTER_BOUND('',#1010,.T.);
#827=FACE_OUTER_BOUND('',#1011,.T.);
#828=FACE_OUTER_BOUND('',#1012,.T.);
#829=FACE_OUTER_BOUND('',#1013,.T.);
#830=FACE_OUTER_BOUND('',#1014,.T.);
#831=FACE_OUTER_BOUND('',#1015,.T.);
#832=FACE_OUTER_BOUND('',#1016,.T.);
#833=FACE_OUTER_BOUND('',#1017,.T.);
#834=FACE_OUTER_BOUND('',#1018,.T.);
#835=FACE_OUTER_BOUND('',#1019,.T.);
#836=FACE_OUTER_BOUND('',#1020,.T.);
#837=FACE_OUTER_BOUND('',#1021,.T.);
#838=FACE_OUTER_BOUND('',#1022,.T.);
#839=FACE_OUTER_BOUND('',#1023,.T.);
#840=FACE_OUTER_BOUND('',#1024,.T.);
#841=FACE_OUTER_BOUND('',#1025,.T.);
#842=FACE_OUTER_BOUND('',#1026,.T.);
#843=FACE_OUTER_BOUND('',#1027,.T.);
#844=FACE_OUTER_BOUND('',#1028,.T.);
#845=FACE_OUTER_BOUND('',#1029,.T.);
#846=FACE_OUTER_BOUND('',#1030,.T.);
#847=FACE_OUTER_BOUND('',#1031,.T.);
#848=FACE_OUTER_BOUND('',#1032,.T.);
#849=FACE_OUTER_BOUND('',#1033,.T.);
#850=FACE_OUTER_BOUND('',#1034,.T.);
#851=FACE_OUTER_BOUND('',#1035,.T.);
#852=FACE_OUTER_BOUND('',#1036,.T.);
#853=FACE_OUTER_BOUND('',#1037,.T.);
#854=FACE_OUTER_BOUND('',#1038,.T.);
#855=FACE_OUTER_BOUND('',#1039,.T.);
#856=FACE_OUTER_BOUND('',#1040,.T.);
#857=FACE_OUTER_BOUND('',#1041,.T.);
#858=FACE_OUTER_BOUND('',#1042,.T.);
#859=FACE_OUTER_BOUND('',#1043,.T.);
#860=FACE_OUTER_BOUND('',#1044,.T.);
#861=FACE_OUTER_BOUND('',#1045,.T.);
#862=FACE_OUTER_BOUND('',#1046,.T.);
#863=FACE_OUTER_BOUND('',#1047,.T.);
#864=FACE_OUTER_BOUND('',#1048,.T.);
#865=FACE_OUTER_BOUND('',#1049,.T.);
#866=FACE_OUTER_BOUND('',#1050,.T.);
#867=FACE_OUTER_BOUND('',#1051,.T.);
#868=FACE_OUTER_BOUND('',#1052,.T.);
#869=FACE_OUTER_BOUND('',#1053,.T.);
#870=FACE_OUTER_BOUND('',#1054,.T.);
#871=FACE_OUTER_BOUND('',#1055,.T.);
#872=FACE_OUTER_BOUND('',#1056,.T.);
#873=FACE_OUTER_BOUND('',#1057,.T.);
#874=FACE_OUTER_BOUND('',#1058,.T.);
#1003=EDGE_LOOP('',(#2574,#2575,#2576,#2577));
#1004=EDGE_LOOP('',(#2578,#2579,#2580,#2581));
#1005=EDGE_LOOP('',(#2582,#2583,#2584,#2585));
#1006=EDGE_LOOP('',(#2586,#2587,#2588,#2589));
#1007=EDGE_LOOP('',(#2590,#2591,#2592,#2593));
#1008=EDGE_LOOP('',(#2594,#2595,#2596,#2597));
#1009=EDGE_LOOP('',(#2598,#2599,#2600,#2601));
#1010=EDGE_LOOP('',(#2602,#2603,#2604,#2605));
#1011=EDGE_LOOP('',(#2606,#2607,#2608,#2609));
#1012=EDGE_LOOP('',(#2610,#2611,#2612,#2613));
#1013=EDGE_LOOP('',(#2614,#2615,#2616,#2617));
#1014=EDGE_LOOP('',(#2618,#2619,#2620,#2621));
#1015=EDGE_LOOP('',(#2622,#2623,#2624,#2625));
#1016=EDGE_LOOP('',(#2626,#2627,#2628,#2629));
#1017=EDGE_LOOP('',(#2630,#2631,#2632,#2633));
#1018=EDGE_LOOP('',(#2634,#2635,#2636,#2637));
#1019=EDGE_LOOP('',(#2638,#2639,#2640,#2641));
#1020=EDGE_LOOP('',(#2642,#2643,#2644,#2645));
#1021=EDGE_LOOP('',(#2646,#2647,#2648,#2649));
#1022=EDGE_LOOP('',(#2650,#2651,#2652,#2653));
#1023=EDGE_LOOP('',(#2654,#2655,#2656,#2657));
#1024=EDGE_LOOP('',(#2658,#2659,#2660,#2661));
#1025=EDGE_LOOP('',(#2662,#2663,#2664,#2665));
#1026=EDGE_LOOP('',(#2666,#2667,#2668,#2669));
#1027=EDGE_LOOP('',(#2670,#2671,#2672,#2673,#2674,#2675,#2676,#2677,#2678,
#2679,#2680,#2681,#2682,#2683,#2684,#2685,#2686,#2687,#2688,#2689,#2690,
#2691,#2692,#2693,#2694,#2695,#2696,#2697,#2698,#2699,#2700,#2701,#2702,
#2703,#2704,#2705,#2706,#2707,#2708,#2709,#2710,#2711,#2712,#2713,#2714,
#2715,#2716,#2717,#2718,#2719,#2720,#2721,#2722,#2723));
#1028=EDGE_LOOP('',(#2724,#2725,#2726,#2727));
#1029=EDGE_LOOP('',(#2728,#2729,#2730,#2731));
#1030=EDGE_LOOP('',(#2732,#2733,#2734,#2735));
#1031=EDGE_LOOP('',(#2736,#2737,#2738,#2739));
#1032=EDGE_LOOP('',(#2740,#2741,#2742,#2743));
#1033=EDGE_LOOP('',(#2744,#2745,#2746,#2747));
#1034=EDGE_LOOP('',(#2748,#2749,#2750,#2751));
#1035=EDGE_LOOP('',(#2752,#2753,#2754,#2755));
#1036=EDGE_LOOP('',(#2756,#2757,#2758,#2759));
#1037=EDGE_LOOP('',(#2760,#2761,#2762,#2763));
#1038=EDGE_LOOP('',(#2764,#2765,#2766,#2767));
#1039=EDGE_LOOP('',(#2768,#2769,#2770,#2771));
#1040=EDGE_LOOP('',(#2772,#2773,#2774,#2775));
#1041=EDGE_LOOP('',(#2776,#2777,#2778,#2779));
#1042=EDGE_LOOP('',(#2780,#2781,#2782,#2783));
#1043=EDGE_LOOP('',(#2784,#2785,#2786,#2787));
#1044=EDGE_LOOP('',(#2788,#2789,#2790,#2791));
#1045=EDGE_LOOP('',(#2792,#2793,#2794,#2795));
#1046=EDGE_LOOP('',(#2796,#2797,#2798,#2799));
#1047=EDGE_LOOP('',(#2800,#2801,#2802,#2803));
#1048=EDGE_LOOP('',(#2804,#2805,#2806,#2807));
#1049=EDGE_LOOP('',(#2808,#2809,#2810,#2811));
#1050=EDGE_LOOP('',(#2812,#2813,#2814,#2815));
#1051=EDGE_LOOP('',(#2816,#2817,#2818,#2819));
#1052=EDGE_LOOP('',(#2820,#2821,#2822,#2823,#2824,#2825));
#1053=EDGE_LOOP('',(#2826,#2827,#2828,#2829));
#1054=EDGE_LOOP('',(#2830));
#1055=EDGE_LOOP('',(#2831));
#1056=EDGE_LOOP('',(#2832,#2833,#2834,#2835));
#1057=EDGE_LOOP('',(#2836,#2837,#2838,#2839,#2840,#2841,#2842,#2843,#2844,
#2845,#2846,#2847,#2848,#2849,#2850,#2851,#2852,#2853,#2854,#2855,#2856,
#2857,#2858,#2859,#2860,#2861,#2862,#2863,#2864,#2865,#2866,#2867,#2868,
#2869,#2870,#2871,#2872,#2873,#2874,#2875,#2876,#2877,#2878,#2879,#2880,
#2881,#2882,#2883,#2884,#2885,#2886,#2887,#2888,#2889));
#1058=EDGE_LOOP('',(#2890,#2891,#2892,#2893));
#1200=CIRCLE('',#3553,9.50579594738959);
#1201=CIRCLE('',#3554,11.0246348408465);
#1202=CIRCLE('',#3555,11.0246348408465);
#1203=CIRCLE('',#3556,11.0246348408465);
#1204=CIRCLE('',#3557,11.0246348408465);
#1205=CIRCLE('',#3558,11.0246348408465);
#1206=CIRCLE('',#3559,11.0246348408465);
#1207=CIRCLE('',#3560,11.0246348408465);
#1208=CIRCLE('',#3561,11.0246348408465);
#1209=CIRCLE('',#3562,11.0246348408465);
#1210=CIRCLE('',#3563,11.0246348408465);
#1211=CIRCLE('',#3564,11.0246348408465);
#1212=CIRCLE('',#3565,11.0246348408465);
#1213=CIRCLE('',#3566,11.0246348408465);
#1214=CIRCLE('',#3567,11.0246348408465);
#1215=CIRCLE('',#3568,11.0246348408465);
#1216=CIRCLE('',#3569,11.0246348408465);
#1217=CIRCLE('',#3570,11.0246348408465);
#1218=CIRCLE('',#3571,11.0246348408465);
#1219=CIRCLE('',#3572,11.0246348408465);
#1220=CIRCLE('',#3573,11.0246348408465);
#1221=CIRCLE('',#3574,11.0246348408465);
#1222=CIRCLE('',#3575,11.0246348408465);
#1223=CIRCLE('',#3576,11.0246348408465);
#1224=CIRCLE('',#3577,11.0246348408465);
#1225=CIRCLE('',#3578,11.0246348408465);
#1226=CIRCLE('',#3580,11.0246348408465);
#1227=CIRCLE('',#3582,11.0246348408465);
#1228=CIRCLE('',#3584,11.0246348408465);
#1229=CIRCLE('',#3586,11.0246348408465);
#1230=CIRCLE('',#3588,11.0246348408465);
#1231=CIRCLE('',#3590,11.0246348408465);
#1232=CIRCLE('',#3592,11.0246348408465);
#1233=CIRCLE('',#3594,11.0246348408465);
#1234=CIRCLE('',#3596,11.0246348408465);
#1235=CIRCLE('',#3598,11.0246348408465);
#1236=CIRCLE('',#3600,11.0246348408465);
#1237=CIRCLE('',#3602,11.0246348408465);
#1238=CIRCLE('',#3604,11.0246348408465);
#1239=CIRCLE('',#3606,11.0246348408465);
#1240=CIRCLE('',#3608,11.0246348408465);
#1241=CIRCLE('',#3610,11.0246348408465);
#1242=CIRCLE('',#3612,11.0246348408465);
#1243=CIRCLE('',#3614,11.0246348408465);
#1244=CIRCLE('',#3616,11.0246348408465);
#1245=CIRCLE('',#3618,11.0246348408465);
#1246=CIRCLE('',#3620,11.0246348408465);
#1247=CIRCLE('',#3622,11.0246348408465);
#1248=CIRCLE('',#3624,11.0246348408465);
#1249=CIRCLE('',#3626,11.0246348408465);
#1250=CIRCLE('',#3629,9.50579594738959);
#1251=CIRCLE('',#3632,9.50579594738959);
#1252=CIRCLE('',#3634,9.50579594738959);
#1253=CIRCLE('',#3636,11.0246348408465);
#1453=VERTEX_POINT('',#6049);
#1454=VERTEX_POINT('',#6050);
#1455=VERTEX_POINT('',#6065);
#1456=VERTEX_POINT('',#6067);
#1457=VERTEX_POINT('',#6084);
#1458=VERTEX_POINT('',#6085);
#1459=VERTEX_POINT('',#6100);
#1460=VERTEX_POINT('',#6102);
#1461=VERTEX_POINT('',#6119);
#1462=VERTEX_POINT('',#6120);
#1463=VERTEX_POINT('',#6135);
#1464=VERTEX_POINT('',#6137);
#1465=VERTEX_POINT('',#6154);
#1466=VERTEX_POINT('',#6155);
#1467=VERTEX_POINT('',#6170);
#1468=VERTEX_POINT('',#6172);
#1469=VERTEX_POINT('',#6189);
#1470=VERTEX_POINT('',#6190);
#1471=VERTEX_POINT('',#6205);
#1472=VERTEX_POINT('',#6207);
#1473=VERTEX_POINT('',#6224);
#1474=VERTEX_POINT('',#6225);
#1475=VERTEX_POINT('',#6240);
#1476=VERTEX_POINT('',#6242);
#1477=VERTEX_POINT('',#6259);
#1478=VERTEX_POINT('',#6260);
#1479=VERTEX_POINT('',#6275);
#1480=VERTEX_POINT('',#6277);
#1481=VERTEX_POINT('',#6294);
#1482=VERTEX_POINT('',#6295);
#1483=VERTEX_POINT('',#6310);
#1484=VERTEX_POINT('',#6312);
#1485=VERTEX_POINT('',#6329);
#1486=VERTEX_POINT('',#6330);
#1487=VERTEX_POINT('',#6345);
#1488=VERTEX_POINT('',#6347);
#1489=VERTEX_POINT('',#6364);
#1490=VERTEX_POINT('',#6365);
#1491=VERTEX_POINT('',#6380);
#1492=VERTEX_POINT('',#6382);
#1493=VERTEX_POINT('',#6399);
#1494=VERTEX_POINT('',#6400);
#1495=VERTEX_POINT('',#6415);
#1496=VERTEX_POINT('',#6417);
#1497=VERTEX_POINT('',#6434);
#1498=VERTEX_POINT('',#6435);
#1499=VERTEX_POINT('',#6450);
#1500=VERTEX_POINT('',#6452);
#1501=VERTEX_POINT('',#6469);
#1502=VERTEX_POINT('',#6470);
#1503=VERTEX_POINT('',#6485);
#1504=VERTEX_POINT('',#6487);
#1505=VERTEX_POINT('',#6504);
#1506=VERTEX_POINT('',#6505);
#1507=VERTEX_POINT('',#6520);
#1508=VERTEX_POINT('',#6522);
#1509=VERTEX_POINT('',#6539);
#1510=VERTEX_POINT('',#6540);
#1511=VERTEX_POINT('',#6555);
#1512=VERTEX_POINT('',#6557);
#1513=VERTEX_POINT('',#6574);
#1514=VERTEX_POINT('',#6575);
#1515=VERTEX_POINT('',#6590);
#1516=VERTEX_POINT('',#6592);
#1517=VERTEX_POINT('',#6609);
#1518=VERTEX_POINT('',#6610);
#1519=VERTEX_POINT('',#6625);
#1520=VERTEX_POINT('',#6627);
#1521=VERTEX_POINT('',#6644);
#1522=VERTEX_POINT('',#6645);
#1523=VERTEX_POINT('',#6660);
#1524=VERTEX_POINT('',#6662);
#1525=VERTEX_POINT('',#6679);
#1526=VERTEX_POINT('',#6680);
#1527=VERTEX_POINT('',#6695);
#1528=VERTEX_POINT('',#6697);
#1529=VERTEX_POINT('',#6714);
#1530=VERTEX_POINT('',#6715);
#1531=VERTEX_POINT('',#6730);
#1532=VERTEX_POINT('',#6732);
#1533=VERTEX_POINT('',#6749);
#1534=VERTEX_POINT('',#6750);
#1535=VERTEX_POINT('',#6765);
#1536=VERTEX_POINT('',#6767);
#1537=VERTEX_POINT('',#6784);
#1538=VERTEX_POINT('',#6785);
#1539=VERTEX_POINT('',#6800);
#1540=VERTEX_POINT('',#6802);
#1541=VERTEX_POINT('',#6819);
#1542=VERTEX_POINT('',#6820);
#1543=VERTEX_POINT('',#6835);
#1544=VERTEX_POINT('',#6837);
#1545=VERTEX_POINT('',#6854);
#1546=VERTEX_POINT('',#6855);
#1547=VERTEX_POINT('',#6870);
#1548=VERTEX_POINT('',#6872);
#1549=VERTEX_POINT('',#6889);
#1550=VERTEX_POINT('',#6891);
#1551=VERTEX_POINT('',#6893);
#1552=VERTEX_POINT('',#6926);
#1553=VERTEX_POINT('',#6937);
#1554=VERTEX_POINT('',#6941);
#1555=VERTEX_POINT('',#6989);
#1556=VERTEX_POINT('',#7007);
#1557=VERTEX_POINT('',#7012);
#1558=VERTEX_POINT('',#7015);
#1853=EDGE_CURVE('',#1453,#1454,#168,.T.);
#1854=EDGE_CURVE('',#1455,#1453,#312,.T.);
#1855=EDGE_CURVE('',#1456,#1455,#169,.T.);
#1856=EDGE_CURVE('',#1454,#1456,#313,.T.);
#1857=EDGE_CURVE('',#1457,#1458,#170,.T.);
#1858=EDGE_CURVE('',#1459,#1457,#314,.T.);
#1859=EDGE_CURVE('',#1460,#1459,#171,.T.);
#1860=EDGE_CURVE('',#1458,#1460,#315,.T.);
#1861=EDGE_CURVE('',#1461,#1462,#172,.T.);
#1862=EDGE_CURVE('',#1463,#1461,#316,.T.);
#1863=EDGE_CURVE('',#1464,#1463,#173,.T.);
#1864=EDGE_CURVE('',#1462,#1464,#317,.T.);
#1865=EDGE_CURVE('',#1465,#1466,#174,.T.);
#1866=EDGE_CURVE('',#1467,#1465,#318,.T.);
#1867=EDGE_CURVE('',#1468,#1467,#175,.T.);
#1868=EDGE_CURVE('',#1466,#1468,#319,.T.);
#1869=EDGE_CURVE('',#1469,#1470,#176,.T.);
#1870=EDGE_CURVE('',#1471,#1469,#320,.T.);
#1871=EDGE_CURVE('',#1472,#1471,#177,.T.);
#1872=EDGE_CURVE('',#1470,#1472,#321,.T.);
#1873=EDGE_CURVE('',#1473,#1474,#178,.T.);
#1874=EDGE_CURVE('',#1475,#1473,#322,.T.);
#1875=EDGE_CURVE('',#1476,#1475,#179,.T.);
#1876=EDGE_CURVE('',#1474,#1476,#323,.T.);
#1877=EDGE_CURVE('',#1477,#1478,#180,.T.);
#1878=EDGE_CURVE('',#1479,#1477,#324,.T.);
#1879=EDGE_CURVE('',#1480,#1479,#181,.T.);
#1880=EDGE_CURVE('',#1478,#1480,#325,.T.);
#1881=EDGE_CURVE('',#1481,#1482,#182,.T.);
#1882=EDGE_CURVE('',#1483,#1481,#326,.T.);
#1883=EDGE_CURVE('',#1484,#1483,#183,.T.);
#1884=EDGE_CURVE('',#1482,#1484,#327,.T.);
#1885=EDGE_CURVE('',#1485,#1486,#184,.T.);
#1886=EDGE_CURVE('',#1487,#1485,#328,.T.);
#1887=EDGE_CURVE('',#1488,#1487,#185,.T.);
#1888=EDGE_CURVE('',#1486,#1488,#329,.T.);
#1889=EDGE_CURVE('',#1489,#1490,#186,.T.);
#1890=EDGE_CURVE('',#1491,#1489,#330,.T.);
#1891=EDGE_CURVE('',#1492,#1491,#187,.T.);
#1892=EDGE_CURVE('',#1490,#1492,#331,.T.);
#1893=EDGE_CURVE('',#1493,#1494,#188,.T.);
#1894=EDGE_CURVE('',#1495,#1493,#332,.T.);
#1895=EDGE_CURVE('',#1496,#1495,#189,.T.);
#1896=EDGE_CURVE('',#1494,#1496,#333,.T.);
#1897=EDGE_CURVE('',#1497,#1498,#190,.T.);
#1898=EDGE_CURVE('',#1499,#1497,#334,.T.);
#1899=EDGE_CURVE('',#1500,#1499,#191,.T.);
#1900=EDGE_CURVE('',#1498,#1500,#335,.T.);
#1901=EDGE_CURVE('',#1501,#1502,#192,.T.);
#1902=EDGE_CURVE('',#1503,#1501,#336,.T.);
#1903=EDGE_CURVE('',#1504,#1503,#193,.T.);
#1904=EDGE_CURVE('',#1502,#1504,#337,.T.);
#1905=EDGE_CURVE('',#1505,#1506,#194,.T.);
#1906=EDGE_CURVE('',#1507,#1505,#338,.T.);
#1907=EDGE_CURVE('',#1508,#1507,#195,.T.);
#1908=EDGE_CURVE('',#1506,#1508,#339,.T.);
#1909=EDGE_CURVE('',#1509,#1510,#196,.T.);
#1910=EDGE_CURVE('',#1511,#1509,#340,.T.);
#1911=EDGE_CURVE('',#1512,#1511,#197,.T.);
#1912=EDGE_CURVE('',#1510,#1512,#341,.T.);
#1913=EDGE_CURVE('',#1513,#1514,#198,.T.);
#1914=EDGE_CURVE('',#1515,#1513,#342,.T.);
#1915=EDGE_CURVE('',#1516,#1515,#199,.T.);
#1916=EDGE_CURVE('',#1514,#1516,#343,.T.);
#1917=EDGE_CURVE('',#1517,#1518,#200,.T.);
#1918=EDGE_CURVE('',#1519,#1517,#344,.T.);
#1919=EDGE_CURVE('',#1520,#1519,#201,.T.);
#1920=EDGE_CURVE('',#1518,#1520,#345,.T.);
#1921=EDGE_CURVE('',#1521,#1522,#202,.T.);
#1922=EDGE_CURVE('',#1523,#1521,#346,.T.);
#1923=EDGE_CURVE('',#1524,#1523,#203,.T.);
#1924=EDGE_CURVE('',#1522,#1524,#347,.T.);
#1925=EDGE_CURVE('',#1525,#1526,#204,.T.);
#1926=EDGE_CURVE('',#1527,#1525,#348,.T.);
#1927=EDGE_CURVE('',#1528,#1527,#205,.T.);
#1928=EDGE_CURVE('',#1526,#1528,#349,.T.);
#1929=EDGE_CURVE('',#1529,#1530,#206,.T.);
#1930=EDGE_CURVE('',#1531,#1529,#350,.T.);
#1931=EDGE_CURVE('',#1532,#1531,#207,.T.);
#1932=EDGE_CURVE('',#1530,#1532,#351,.T.);
#1933=EDGE_CURVE('',#1533,#1534,#208,.T.);
#1934=EDGE_CURVE('',#1535,#1533,#352,.T.);
#1935=EDGE_CURVE('',#1536,#1535,#209,.T.);
#1936=EDGE_CURVE('',#1534,#1536,#353,.T.);
#1937=EDGE_CURVE('',#1537,#1538,#210,.T.);
#1938=EDGE_CURVE('',#1539,#1537,#354,.T.);
#1939=EDGE_CURVE('',#1540,#1539,#211,.T.);
#1940=EDGE_CURVE('',#1538,#1540,#355,.T.);
#1941=EDGE_CURVE('',#1541,#1542,#212,.T.);
#1942=EDGE_CURVE('',#1543,#1541,#356,.T.);
#1943=EDGE_CURVE('',#1544,#1543,#213,.T.);
#1944=EDGE_CURVE('',#1542,#1544,#357,.T.);
#1945=EDGE_CURVE('',#1545,#1546,#214,.T.);
#1946=EDGE_CURVE('',#1547,#1545,#358,.T.);
#1947=EDGE_CURVE('',#1548,#1547,#215,.T.);
#1948=EDGE_CURVE('',#1546,#1548,#359,.T.);
#1949=EDGE_CURVE('',#1549,#1549,#1200,.T.);
#1950=EDGE_CURVE('',#1549,#1550,#360,.T.);
#1951=EDGE_CURVE('',#1550,#1551,#216,.T.);
#1952=EDGE_CURVE('',#1551,#1548,#1201,.T.);
#1953=EDGE_CURVE('',#1547,#1544,#1202,.T.);
#1954=EDGE_CURVE('',#1543,#1540,#1203,.T.);
#1955=EDGE_CURVE('',#1539,#1536,#1204,.T.);
#1956=EDGE_CURVE('',#1535,#1532,#1205,.T.);
#1957=EDGE_CURVE('',#1531,#1528,#1206,.T.);
#1958=EDGE_CURVE('',#1527,#1524,#1207,.T.);
#1959=EDGE_CURVE('',#1523,#1520,#1208,.T.);
#1960=EDGE_CURVE('',#1519,#1516,#1209,.T.);
#1961=EDGE_CURVE('',#1515,#1512,#1210,.T.);
#1962=EDGE_CURVE('',#1511,#1508,#1211,.T.);
#1963=EDGE_CURVE('',#1507,#1504,#1212,.T.);
#1964=EDGE_CURVE('',#1503,#1500,#1213,.T.);
#1965=EDGE_CURVE('',#1499,#1496,#1214,.T.);
#1966=EDGE_CURVE('',#1495,#1492,#1215,.T.);
#1967=EDGE_CURVE('',#1491,#1488,#1216,.T.);
#1968=EDGE_CURVE('',#1487,#1484,#1217,.T.);
#1969=EDGE_CURVE('',#1483,#1480,#1218,.T.);
#1970=EDGE_CURVE('',#1479,#1476,#1219,.T.);
#1971=EDGE_CURVE('',#1475,#1472,#1220,.T.);
#1972=EDGE_CURVE('',#1471,#1468,#1221,.T.);
#1973=EDGE_CURVE('',#1467,#1464,#1222,.T.);
#1974=EDGE_CURVE('',#1463,#1460,#1223,.T.);
#1975=EDGE_CURVE('',#1459,#1456,#1224,.T.);
#1976=EDGE_CURVE('',#1455,#1552,#1225,.T.);
#1977=EDGE_CURVE('',#1552,#1550,#217,.T.);
#1978=EDGE_CURVE('',#1453,#1553,#1226,.T.);
#1979=EDGE_CURVE('',#1553,#1552,#361,.T.);
#1980=EDGE_CURVE('',#1551,#1554,#362,.T.);
#1981=EDGE_CURVE('',#1554,#1546,#1227,.T.);
#1982=EDGE_CURVE('',#1545,#1542,#1228,.T.);
#1983=EDGE_CURVE('',#1541,#1538,#1229,.T.);
#1984=EDGE_CURVE('',#1537,#1534,#1230,.T.);
#1985=EDGE_CURVE('',#1533,#1530,#1231,.T.);
#1986=EDGE_CURVE('',#1529,#1526,#1232,.T.);
#1987=EDGE_CURVE('',#1525,#1522,#1233,.T.);
#1988=EDGE_CURVE('',#1521,#1518,#1234,.T.);
#1989=EDGE_CURVE('',#1517,#1514,#1235,.T.);
#1990=EDGE_CURVE('',#1513,#1510,#1236,.T.);
#1991=EDGE_CURVE('',#1509,#1506,#1237,.T.);
#1992=EDGE_CURVE('',#1505,#1502,#1238,.T.);
#1993=EDGE_CURVE('',#1501,#1498,#1239,.T.);
#1994=EDGE_CURVE('',#1497,#1494,#1240,.T.);
#1995=EDGE_CURVE('',#1493,#1490,#1241,.T.);
#1996=EDGE_CURVE('',#1489,#1486,#1242,.T.);
#1997=EDGE_CURVE('',#1485,#1482,#1243,.T.);
#1998=EDGE_CURVE('',#1481,#1478,#1244,.T.);
#1999=EDGE_CURVE('',#1477,#1474,#1245,.T.);
#2000=EDGE_CURVE('',#1473,#1470,#1246,.T.);
#2001=EDGE_CURVE('',#1469,#1466,#1247,.T.);
#2002=EDGE_CURVE('',#1465,#1462,#1248,.T.);
#2003=EDGE_CURVE('',#1461,#1458,#1249,.T.);
#2004=EDGE_CURVE('',#1554,#1555,#218,.T.);
#2005=EDGE_CURVE('',#1555,#1553,#219,.T.);
#2006=EDGE_CURVE('',#1556,#1556,#1250,.T.);
#2007=EDGE_CURVE('',#1556,#1549,#363,.T.);
#2008=EDGE_CURVE('',#1557,#1557,#1251,.T.);
#2009=EDGE_CURVE('',#1558,#1558,#1252,.T.);
#2010=EDGE_CURVE('',#1558,#1557,#364,.T.);
#2011=EDGE_CURVE('',#1457,#1454,#1253,.T.);
#2012=EDGE_CURVE('',#1555,#1558,#365,.T.);
#2574=ORIENTED_EDGE('',*,*,#1853,.F.);
#2575=ORIENTED_EDGE('',*,*,#1854,.F.);
#2576=ORIENTED_EDGE('',*,*,#1855,.F.);
#2577=ORIENTED_EDGE('',*,*,#1856,.F.);
#2578=ORIENTED_EDGE('',*,*,#1857,.F.);
#2579=ORIENTED_EDGE('',*,*,#1858,.F.);
#2580=ORIENTED_EDGE('',*,*,#1859,.F.);
#2581=ORIENTED_EDGE('',*,*,#1860,.F.);
#2582=ORIENTED_EDGE('',*,*,#1861,.F.);
#2583=ORIENTED_EDGE('',*,*,#1862,.F.);
#2584=ORIENTED_EDGE('',*,*,#1863,.F.);
#2585=ORIENTED_EDGE('',*,*,#1864,.F.);
#2586=ORIENTED_EDGE('',*,*,#1865,.F.);
#2587=ORIENTED_EDGE('',*,*,#1866,.F.);
#2588=ORIENTED_EDGE('',*,*,#1867,.F.);
#2589=ORIENTED_EDGE('',*,*,#1868,.F.);
#2590=ORIENTED_EDGE('',*,*,#1869,.F.);
#2591=ORIENTED_EDGE('',*,*,#1870,.F.);
#2592=ORIENTED_EDGE('',*,*,#1871,.F.);
#2593=ORIENTED_EDGE('',*,*,#1872,.F.);
#2594=ORIENTED_EDGE('',*,*,#1873,.F.);
#2595=ORIENTED_EDGE('',*,*,#1874,.F.);
#2596=ORIENTED_EDGE('',*,*,#1875,.F.);
#2597=ORIENTED_EDGE('',*,*,#1876,.F.);
#2598=ORIENTED_EDGE('',*,*,#1877,.F.);
#2599=ORIENTED_EDGE('',*,*,#1878,.F.);
#2600=ORIENTED_EDGE('',*,*,#1879,.F.);
#2601=ORIENTED_EDGE('',*,*,#1880,.F.);
#2602=ORIENTED_EDGE('',*,*,#1881,.F.);
#2603=ORIENTED_EDGE('',*,*,#1882,.F.);
#2604=ORIENTED_EDGE('',*,*,#1883,.F.);
#2605=ORIENTED_EDGE('',*,*,#1884,.F.);
#2606=ORIENTED_EDGE('',*,*,#1885,.F.);
#2607=ORIENTED_EDGE('',*,*,#1886,.F.);
#2608=ORIENTED_EDGE('',*,*,#1887,.F.);
#2609=ORIENTED_EDGE('',*,*,#1888,.F.);
#2610=ORIENTED_EDGE('',*,*,#1889,.F.);
#2611=ORIENTED_EDGE('',*,*,#1890,.F.);
#2612=ORIENTED_EDGE('',*,*,#1891,.F.);
#2613=ORIENTED_EDGE('',*,*,#1892,.F.);
#2614=ORIENTED_EDGE('',*,*,#1893,.F.);
#2615=ORIENTED_EDGE('',*,*,#1894,.F.);
#2616=ORIENTED_EDGE('',*,*,#1895,.F.);
#2617=ORIENTED_EDGE('',*,*,#1896,.F.);
#2618=ORIENTED_EDGE('',*,*,#1897,.F.);
#2619=ORIENTED_EDGE('',*,*,#1898,.F.);
#2620=ORIENTED_EDGE('',*,*,#1899,.F.);
#2621=ORIENTED_EDGE('',*,*,#1900,.F.);
#2622=ORIENTED_EDGE('',*,*,#1901,.F.);
#2623=ORIENTED_EDGE('',*,*,#1902,.F.);
#2624=ORIENTED_EDGE('',*,*,#1903,.F.);
#2625=ORIENTED_EDGE('',*,*,#1904,.F.);
#2626=ORIENTED_EDGE('',*,*,#1905,.F.);
#2627=ORIENTED_EDGE('',*,*,#1906,.F.);
#2628=ORIENTED_EDGE('',*,*,#1907,.F.);
#2629=ORIENTED_EDGE('',*,*,#1908,.F.);
#2630=ORIENTED_EDGE('',*,*,#1909,.F.);
#2631=ORIENTED_EDGE('',*,*,#1910,.F.);
#2632=ORIENTED_EDGE('',*,*,#1911,.F.);
#2633=ORIENTED_EDGE('',*,*,#1912,.F.);
#2634=ORIENTED_EDGE('',*,*,#1913,.F.);
#2635=ORIENTED_EDGE('',*,*,#1914,.F.);
#2636=ORIENTED_EDGE('',*,*,#1915,.F.);
#2637=ORIENTED_EDGE('',*,*,#1916,.F.);
#2638=ORIENTED_EDGE('',*,*,#1917,.F.);
#2639=ORIENTED_EDGE('',*,*,#1918,.F.);
#2640=ORIENTED_EDGE('',*,*,#1919,.F.);
#2641=ORIENTED_EDGE('',*,*,#1920,.F.);
#2642=ORIENTED_EDGE('',*,*,#1921,.F.);
#2643=ORIENTED_EDGE('',*,*,#1922,.F.);
#2644=ORIENTED_EDGE('',*,*,#1923,.F.);
#2645=ORIENTED_EDGE('',*,*,#1924,.F.);
#2646=ORIENTED_EDGE('',*,*,#1925,.F.);
#2647=ORIENTED_EDGE('',*,*,#1926,.F.);
#2648=ORIENTED_EDGE('',*,*,#1927,.F.);
#2649=ORIENTED_EDGE('',*,*,#1928,.F.);
#2650=ORIENTED_EDGE('',*,*,#1929,.F.);
#2651=ORIENTED_EDGE('',*,*,#1930,.F.);
#2652=ORIENTED_EDGE('',*,*,#1931,.F.);
#2653=ORIENTED_EDGE('',*,*,#1932,.F.);
#2654=ORIENTED_EDGE('',*,*,#1933,.F.);
#2655=ORIENTED_EDGE('',*,*,#1934,.F.);
#2656=ORIENTED_EDGE('',*,*,#1935,.F.);
#2657=ORIENTED_EDGE('',*,*,#1936,.F.);
#2658=ORIENTED_EDGE('',*,*,#1937,.F.);
#2659=ORIENTED_EDGE('',*,*,#1938,.F.);
#2660=ORIENTED_EDGE('',*,*,#1939,.F.);
#2661=ORIENTED_EDGE('',*,*,#1940,.F.);
#2662=ORIENTED_EDGE('',*,*,#1941,.F.);
#2663=ORIENTED_EDGE('',*,*,#1942,.F.);
#2664=ORIENTED_EDGE('',*,*,#1943,.F.);
#2665=ORIENTED_EDGE('',*,*,#1944,.F.);
#2666=ORIENTED_EDGE('',*,*,#1945,.F.);
#2667=ORIENTED_EDGE('',*,*,#1946,.F.);
#2668=ORIENTED_EDGE('',*,*,#1947,.F.);
#2669=ORIENTED_EDGE('',*,*,#1948,.F.);
#2670=ORIENTED_EDGE('',*,*,#1949,.F.);
#2671=ORIENTED_EDGE('',*,*,#1950,.T.);
#2672=ORIENTED_EDGE('',*,*,#1951,.T.);
#2673=ORIENTED_EDGE('',*,*,#1952,.T.);
#2674=ORIENTED_EDGE('',*,*,#1947,.T.);
#2675=ORIENTED_EDGE('',*,*,#1953,.T.);
#2676=ORIENTED_EDGE('',*,*,#1943,.T.);
#2677=ORIENTED_EDGE('',*,*,#1954,.T.);
#2678=ORIENTED_EDGE('',*,*,#1939,.T.);
#2679=ORIENTED_EDGE('',*,*,#1955,.T.);
#2680=ORIENTED_EDGE('',*,*,#1935,.T.);
#2681=ORIENTED_EDGE('',*,*,#1956,.T.);
#2682=ORIENTED_EDGE('',*,*,#1931,.T.);
#2683=ORIENTED_EDGE('',*,*,#1957,.T.);
#2684=ORIENTED_EDGE('',*,*,#1927,.T.);
#2685=ORIENTED_EDGE('',*,*,#1958,.T.);
#2686=ORIENTED_EDGE('',*,*,#1923,.T.);
#2687=ORIENTED_EDGE('',*,*,#1959,.T.);
#2688=ORIENTED_EDGE('',*,*,#1919,.T.);
#2689=ORIENTED_EDGE('',*,*,#1960,.T.);
#2690=ORIENTED_EDGE('',*,*,#1915,.T.);
#2691=ORIENTED_EDGE('',*,*,#1961,.T.);
#2692=ORIENTED_EDGE('',*,*,#1911,.T.);
#2693=ORIENTED_EDGE('',*,*,#1962,.T.);
#2694=ORIENTED_EDGE('',*,*,#1907,.T.);
#2695=ORIENTED_EDGE('',*,*,#1963,.T.);
#2696=ORIENTED_EDGE('',*,*,#1903,.T.);
#2697=ORIENTED_EDGE('',*,*,#1964,.T.);
#2698=ORIENTED_EDGE('',*,*,#1899,.T.);
#2699=ORIENTED_EDGE('',*,*,#1965,.T.);
#2700=ORIENTED_EDGE('',*,*,#1895,.T.);
#2701=ORIENTED_EDGE('',*,*,#1966,.T.);
#2702=ORIENTED_EDGE('',*,*,#1891,.T.);
#2703=ORIENTED_EDGE('',*,*,#1967,.T.);
#2704=ORIENTED_EDGE('',*,*,#1887,.T.);
#2705=ORIENTED_EDGE('',*,*,#1968,.T.);
#2706=ORIENTED_EDGE('',*,*,#1883,.T.);
#2707=ORIENTED_EDGE('',*,*,#1969,.T.);
#2708=ORIENTED_EDGE('',*,*,#1879,.T.);
#2709=ORIENTED_EDGE('',*,*,#1970,.T.);
#2710=ORIENTED_EDGE('',*,*,#1875,.T.);
#2711=ORIENTED_EDGE('',*,*,#1971,.T.);
#2712=ORIENTED_EDGE('',*,*,#1871,.T.);
#2713=ORIENTED_EDGE('',*,*,#1972,.T.);
#2714=ORIENTED_EDGE('',*,*,#1867,.T.);
#2715=ORIENTED_EDGE('',*,*,#1973,.T.);
#2716=ORIENTED_EDGE('',*,*,#1863,.T.);
#2717=ORIENTED_EDGE('',*,*,#1974,.T.);
#2718=ORIENTED_EDGE('',*,*,#1859,.T.);
#2719=ORIENTED_EDGE('',*,*,#1975,.T.);
#2720=ORIENTED_EDGE('',*,*,#1855,.T.);
#2721=ORIENTED_EDGE('',*,*,#1976,.T.);
#2722=ORIENTED_EDGE('',*,*,#1977,.T.);
#2723=ORIENTED_EDGE('',*,*,#1950,.F.);
#2724=ORIENTED_EDGE('',*,*,#1854,.T.);
#2725=ORIENTED_EDGE('',*,*,#1978,.T.);
#2726=ORIENTED_EDGE('',*,*,#1979,.T.);
#2727=ORIENTED_EDGE('',*,*,#1976,.F.);
#2728=ORIENTED_EDGE('',*,*,#1948,.T.);
#2729=ORIENTED_EDGE('',*,*,#1952,.F.);
#2730=ORIENTED_EDGE('',*,*,#1980,.T.);
#2731=ORIENTED_EDGE('',*,*,#1981,.T.);
#2732=ORIENTED_EDGE('',*,*,#1944,.T.);
#2733=ORIENTED_EDGE('',*,*,#1953,.F.);
#2734=ORIENTED_EDGE('',*,*,#1946,.T.);
#2735=ORIENTED_EDGE('',*,*,#1982,.T.);
#2736=ORIENTED_EDGE('',*,*,#1940,.T.);
#2737=ORIENTED_EDGE('',*,*,#1954,.F.);
#2738=ORIENTED_EDGE('',*,*,#1942,.T.);
#2739=ORIENTED_EDGE('',*,*,#1983,.T.);
#2740=ORIENTED_EDGE('',*,*,#1936,.T.);
#2741=ORIENTED_EDGE('',*,*,#1955,.F.);
#2742=ORIENTED_EDGE('',*,*,#1938,.T.);
#2743=ORIENTED_EDGE('',*,*,#1984,.T.);
#2744=ORIENTED_EDGE('',*,*,#1932,.T.);
#2745=ORIENTED_EDGE('',*,*,#1956,.F.);
#2746=ORIENTED_EDGE('',*,*,#1934,.T.);
#2747=ORIENTED_EDGE('',*,*,#1985,.T.);
#2748=ORIENTED_EDGE('',*,*,#1928,.T.);
#2749=ORIENTED_EDGE('',*,*,#1957,.F.);
#2750=ORIENTED_EDGE('',*,*,#1930,.T.);
#2751=ORIENTED_EDGE('',*,*,#1986,.T.);
#2752=ORIENTED_EDGE('',*,*,#1924,.T.);
#2753=ORIENTED_EDGE('',*,*,#1958,.F.);
#2754=ORIENTED_EDGE('',*,*,#1926,.T.);
#2755=ORIENTED_EDGE('',*,*,#1987,.T.);
#2756=ORIENTED_EDGE('',*,*,#1920,.T.);
#2757=ORIENTED_EDGE('',*,*,#1959,.F.);
#2758=ORIENTED_EDGE('',*,*,#1922,.T.);
#2759=ORIENTED_EDGE('',*,*,#1988,.T.);
#2760=ORIENTED_EDGE('',*,*,#1916,.T.);
#2761=ORIENTED_EDGE('',*,*,#1960,.F.);
#2762=ORIENTED_EDGE('',*,*,#1918,.T.);
#2763=ORIENTED_EDGE('',*,*,#1989,.T.);
#2764=ORIENTED_EDGE('',*,*,#1912,.T.);
#2765=ORIENTED_EDGE('',*,*,#1961,.F.);
#2766=ORIENTED_EDGE('',*,*,#1914,.T.);
#2767=ORIENTED_EDGE('',*,*,#1990,.T.);
#2768=ORIENTED_EDGE('',*,*,#1908,.T.);
#2769=ORIENTED_EDGE('',*,*,#1962,.F.);
#2770=ORIENTED_EDGE('',*,*,#1910,.T.);
#2771=ORIENTED_EDGE('',*,*,#1991,.T.);
#2772=ORIENTED_EDGE('',*,*,#1904,.T.);
#2773=ORIENTED_EDGE('',*,*,#1963,.F.);
#2774=ORIENTED_EDGE('',*,*,#1906,.T.);
#2775=ORIENTED_EDGE('',*,*,#1992,.T.);
#2776=ORIENTED_EDGE('',*,*,#1900,.T.);
#2777=ORIENTED_EDGE('',*,*,#1964,.F.);
#2778=ORIENTED_EDGE('',*,*,#1902,.T.);
#2779=ORIENTED_EDGE('',*,*,#1993,.T.);
#2780=ORIENTED_EDGE('',*,*,#1896,.T.);
#2781=ORIENTED_EDGE('',*,*,#1965,.F.);
#2782=ORIENTED_EDGE('',*,*,#1898,.T.);
#2783=ORIENTED_EDGE('',*,*,#1994,.T.);
#2784=ORIENTED_EDGE('',*,*,#1892,.T.);
#2785=ORIENTED_EDGE('',*,*,#1966,.F.);
#2786=ORIENTED_EDGE('',*,*,#1894,.T.);
#2787=ORIENTED_EDGE('',*,*,#1995,.T.);
#2788=ORIENTED_EDGE('',*,*,#1888,.T.);
#2789=ORIENTED_EDGE('',*,*,#1967,.F.);
#2790=ORIENTED_EDGE('',*,*,#1890,.T.);
#2791=ORIENTED_EDGE('',*,*,#1996,.T.);
#2792=ORIENTED_EDGE('',*,*,#1884,.T.);
#2793=ORIENTED_EDGE('',*,*,#1968,.F.);
#2794=ORIENTED_EDGE('',*,*,#1886,.T.);
#2795=ORIENTED_EDGE('',*,*,#1997,.T.);
#2796=ORIENTED_EDGE('',*,*,#1880,.T.);
#2797=ORIENTED_EDGE('',*,*,#1969,.F.);
#2798=ORIENTED_EDGE('',*,*,#1882,.T.);
#2799=ORIENTED_EDGE('',*,*,#1998,.T.);
#2800=ORIENTED_EDGE('',*,*,#1876,.T.);
#2801=ORIENTED_EDGE('',*,*,#1970,.F.);
#2802=ORIENTED_EDGE('',*,*,#1878,.T.);
#2803=ORIENTED_EDGE('',*,*,#1999,.T.);
#2804=ORIENTED_EDGE('',*,*,#1872,.T.);
#2805=ORIENTED_EDGE('',*,*,#1971,.F.);
#2806=ORIENTED_EDGE('',*,*,#1874,.T.);
#2807=ORIENTED_EDGE('',*,*,#2000,.T.);
#2808=ORIENTED_EDGE('',*,*,#1868,.T.);
#2809=ORIENTED_EDGE('',*,*,#1972,.F.);
#2810=ORIENTED_EDGE('',*,*,#1870,.T.);
#2811=ORIENTED_EDGE('',*,*,#2001,.T.);
#2812=ORIENTED_EDGE('',*,*,#1864,.T.);
#2813=ORIENTED_EDGE('',*,*,#1973,.F.);
#2814=ORIENTED_EDGE('',*,*,#1866,.T.);
#2815=ORIENTED_EDGE('',*,*,#2002,.T.);
#2816=ORIENTED_EDGE('',*,*,#1860,.T.);
#2817=ORIENTED_EDGE('',*,*,#1974,.F.);
#2818=ORIENTED_EDGE('',*,*,#1862,.T.);
#2819=ORIENTED_EDGE('',*,*,#2003,.T.);
#2820=ORIENTED_EDGE('',*,*,#2004,.F.);
#2821=ORIENTED_EDGE('',*,*,#1980,.F.);
#2822=ORIENTED_EDGE('',*,*,#1951,.F.);
#2823=ORIENTED_EDGE('',*,*,#1977,.F.);
#2824=ORIENTED_EDGE('',*,*,#1979,.F.);
#2825=ORIENTED_EDGE('',*,*,#2005,.F.);
#2826=ORIENTED_EDGE('',*,*,#2006,.F.);
#2827=ORIENTED_EDGE('',*,*,#2007,.T.);
#2828=ORIENTED_EDGE('',*,*,#1949,.T.);
#2829=ORIENTED_EDGE('',*,*,#2007,.F.);
#2830=ORIENTED_EDGE('',*,*,#2006,.T.);
#2831=ORIENTED_EDGE('',*,*,#2008,.F.);
#2832=ORIENTED_EDGE('',*,*,#2009,.F.);
#2833=ORIENTED_EDGE('',*,*,#2010,.T.);
#2834=ORIENTED_EDGE('',*,*,#2008,.T.);
#2835=ORIENTED_EDGE('',*,*,#2010,.F.);
#2836=ORIENTED_EDGE('',*,*,#1853,.T.);
#2837=ORIENTED_EDGE('',*,*,#2011,.F.);
#2838=ORIENTED_EDGE('',*,*,#1857,.T.);
#2839=ORIENTED_EDGE('',*,*,#2003,.F.);
#2840=ORIENTED_EDGE('',*,*,#1861,.T.);
#2841=ORIENTED_EDGE('',*,*,#2002,.F.);
#2842=ORIENTED_EDGE('',*,*,#1865,.T.);
#2843=ORIENTED_EDGE('',*,*,#2001,.F.);
#2844=ORIENTED_EDGE('',*,*,#1869,.T.);
#2845=ORIENTED_EDGE('',*,*,#2000,.F.);
#2846=ORIENTED_EDGE('',*,*,#1873,.T.);
#2847=ORIENTED_EDGE('',*,*,#1999,.F.);
#2848=ORIENTED_EDGE('',*,*,#1877,.T.);
#2849=ORIENTED_EDGE('',*,*,#1998,.F.);
#2850=ORIENTED_EDGE('',*,*,#1881,.T.);
#2851=ORIENTED_EDGE('',*,*,#1997,.F.);
#2852=ORIENTED_EDGE('',*,*,#1885,.T.);
#2853=ORIENTED_EDGE('',*,*,#1996,.F.);
#2854=ORIENTED_EDGE('',*,*,#1889,.T.);
#2855=ORIENTED_EDGE('',*,*,#1995,.F.);
#2856=ORIENTED_EDGE('',*,*,#1893,.T.);
#2857=ORIENTED_EDGE('',*,*,#1994,.F.);
#2858=ORIENTED_EDGE('',*,*,#1897,.T.);
#2859=ORIENTED_EDGE('',*,*,#1993,.F.);
#2860=ORIENTED_EDGE('',*,*,#1901,.T.);
#2861=ORIENTED_EDGE('',*,*,#1992,.F.);
#2862=ORIENTED_EDGE('',*,*,#1905,.T.);
#2863=ORIENTED_EDGE('',*,*,#1991,.F.);
#2864=ORIENTED_EDGE('',*,*,#1909,.T.);
#2865=ORIENTED_EDGE('',*,*,#1990,.F.);
#2866=ORIENTED_EDGE('',*,*,#1913,.T.);
#2867=ORIENTED_EDGE('',*,*,#1989,.F.);
#2868=ORIENTED_EDGE('',*,*,#1917,.T.);
#2869=ORIENTED_EDGE('',*,*,#1988,.F.);
#2870=ORIENTED_EDGE('',*,*,#1921,.T.);
#2871=ORIENTED_EDGE('',*,*,#1987,.F.);
#2872=ORIENTED_EDGE('',*,*,#1925,.T.);
#2873=ORIENTED_EDGE('',*,*,#1986,.F.);
#2874=ORIENTED_EDGE('',*,*,#1929,.T.);
#2875=ORIENTED_EDGE('',*,*,#1985,.F.);
#2876=ORIENTED_EDGE('',*,*,#1933,.T.);
#2877=ORIENTED_EDGE('',*,*,#1984,.F.);
#2878=ORIENTED_EDGE('',*,*,#1937,.T.);
#2879=ORIENTED_EDGE('',*,*,#1983,.F.);
#2880=ORIENTED_EDGE('',*,*,#1941,.T.);
#2881=ORIENTED_EDGE('',*,*,#1982,.F.);
#2882=ORIENTED_EDGE('',*,*,#1945,.T.);
#2883=ORIENTED_EDGE('',*,*,#1981,.F.);
#2884=ORIENTED_EDGE('',*,*,#2004,.T.);
#2885=ORIENTED_EDGE('',*,*,#2012,.T.);
#2886=ORIENTED_EDGE('',*,*,#2009,.T.);
#2887=ORIENTED_EDGE('',*,*,#2012,.F.);
#2888=ORIENTED_EDGE('',*,*,#2005,.T.);
#2889=ORIENTED_EDGE('',*,*,#1978,.F.);
#2890=ORIENTED_EDGE('',*,*,#1856,.T.);
#2891=ORIENTED_EDGE('',*,*,#1975,.F.);
#2892=ORIENTED_EDGE('',*,*,#1858,.T.);
#2893=ORIENTED_EDGE('',*,*,#2011,.T.);
#3123=ADVANCED_FACE('',(#819),#624,.F.);
#3124=ADVANCED_FACE('',(#820),#625,.F.);
#3125=ADVANCED_FACE('',(#821),#626,.F.);
#3126=ADVANCED_FACE('',(#822),#627,.F.);
#3127=ADVANCED_FACE('',(#823),#628,.F.);
#3128=ADVANCED_FACE('',(#824),#629,.F.);
#3129=ADVANCED_FACE('',(#825),#630,.F.);
#3130=ADVANCED_FACE('',(#826),#631,.F.);
#3131=ADVANCED_FACE('',(#827),#632,.F.);
#3132=ADVANCED_FACE('',(#828),#633,.F.);
#3133=ADVANCED_FACE('',(#829),#634,.F.);
#3134=ADVANCED_FACE('',(#830),#635,.F.);
#3135=ADVANCED_FACE('',(#831),#636,.F.);
#3136=ADVANCED_FACE('',(#832),#637,.F.);
#3137=ADVANCED_FACE('',(#833),#638,.F.);
#3138=ADVANCED_FACE('',(#834),#639,.F.);
#3139=ADVANCED_FACE('',(#835),#640,.F.);
#3140=ADVANCED_FACE('',(#836),#641,.F.);
#3141=ADVANCED_FACE('',(#837),#642,.F.);
#3142=ADVANCED_FACE('',(#838),#643,.F.);
#3143=ADVANCED_FACE('',(#839),#644,.F.);
#3144=ADVANCED_FACE('',(#840),#645,.F.);
#3145=ADVANCED_FACE('',(#841),#646,.F.);
#3146=ADVANCED_FACE('',(#842),#647,.F.);
#3147=ADVANCED_FACE('',(#843),#101,.T.);
#3148=ADVANCED_FACE('',(#844),#648,.T.);
#3149=ADVANCED_FACE('',(#845),#649,.T.);
#3150=ADVANCED_FACE('',(#846),#650,.T.);
#3151=ADVANCED_FACE('',(#847),#651,.T.);
#3152=ADVANCED_FACE('',(#848),#652,.T.);
#3153=ADVANCED_FACE('',(#849),#653,.T.);
#3154=ADVANCED_FACE('',(#850),#654,.T.);
#3155=ADVANCED_FACE('',(#851),#655,.T.);
#3156=ADVANCED_FACE('',(#852),#656,.T.);
#3157=ADVANCED_FACE('',(#853),#657,.T.);
#3158=ADVANCED_FACE('',(#854),#658,.T.);
#3159=ADVANCED_FACE('',(#855),#659,.T.);
#3160=ADVANCED_FACE('',(#856),#660,.T.);
#3161=ADVANCED_FACE('',(#857),#661,.T.);
#3162=ADVANCED_FACE('',(#858),#662,.T.);
#3163=ADVANCED_FACE('',(#859),#663,.T.);
#3164=ADVANCED_FACE('',(#860),#664,.T.);
#3165=ADVANCED_FACE('',(#861),#665,.T.);
#3166=ADVANCED_FACE('',(#862),#666,.T.);
#3167=ADVANCED_FACE('',(#863),#667,.T.);
#3168=ADVANCED_FACE('',(#864),#668,.T.);
#3169=ADVANCED_FACE('',(#865),#669,.T.);
#3170=ADVANCED_FACE('',(#866),#670,.T.);
#3171=ADVANCED_FACE('',(#867),#671,.T.);
#3172=ADVANCED_FACE('',(#868),#672,.F.);
#3173=ADVANCED_FACE('',(#869),#673,.T.);
#3174=ADVANCED_FACE('',(#870),#710,.T.);
#3175=ADVANCED_FACE('',(#871),#711,.T.);
#3176=ADVANCED_FACE('',(#872),#674,.T.);
#3177=ADVANCED_FACE('',(#873),#102,.T.);
#3178=ADVANCED_FACE('',(#874),#675,.T.);
#3217=CLOSED_SHELL('',(#3123,#3124,#3125,#3126,#3127,#3128,#3129,#3130,
#3131,#3132,#3133,#3134,#3135,#3136,#3137,#3138,#3139,#3140,#3141,#3142,
#3143,#3144,#3145,#3146,#3147,#3148,#3149,#3150,#3151,#3152,#3153,#3154,
#3155,#3156,#3157,#3158,#3159,#3160,#3161,#3162,#3163,#3164,#3165,#3166,
#3167,#3168,#3169,#3170,#3171,#3172,#3173,#3174,#3175,#3176,#3177,#3178));
#3527=AXIS2_PLACEMENT_3D('',#6047,#4191,#4192);
#3528=AXIS2_PLACEMENT_3D('',#6048,#4193,#4194);
#3529=AXIS2_PLACEMENT_3D('',#6083,#4197,#4198);
#3530=AXIS2_PLACEMENT_3D('',#6118,#4201,#4202);
#3531=AXIS2_PLACEMENT_3D('',#6153,#4205,#4206);
#3532=AXIS2_PLACEMENT_3D('',#6188,#4209,#4210);
#3533=AXIS2_PLACEMENT_3D('',#6223,#4213,#4214);
#3534=AXIS2_PLACEMENT_3D('',#6258,#4217,#4218);
#3535=AXIS2_PLACEMENT_3D('',#6293,#4221,#4222);
#3536=AXIS2_PLACEMENT_3D('',#6328,#4225,#4226);
#3537=AXIS2_PLACEMENT_3D('',#6363,#4229,#4230);
#3538=AXIS2_PLACEMENT_3D('',#6398,#4233,#4234);
#3539=AXIS2_PLACEMENT_3D('',#6433,#4237,#4238);
#3540=AXIS2_PLACEMENT_3D('',#6468,#4241,#4242);
#3541=AXIS2_PLACEMENT_3D('',#6503,#4245,#4246);
#3542=AXIS2_PLACEMENT_3D('',#6538,#4249,#4250);
#3543=AXIS2_PLACEMENT_3D('',#6573,#4253,#4254);
#3544=AXIS2_PLACEMENT_3D('',#6608,#4257,#4258);
#3545=AXIS2_PLACEMENT_3D('',#6643,#4261,#4262);
#3546=AXIS2_PLACEMENT_3D('',#6678,#4265,#4266);
#3547=AXIS2_PLACEMENT_3D('',#6713,#4269,#4270);
#3548=AXIS2_PLACEMENT_3D('',#6748,#4273,#4274);
#3549=AXIS2_PLACEMENT_3D('',#6783,#4277,#4278);
#3550=AXIS2_PLACEMENT_3D('',#6818,#4281,#4282);
#3551=AXIS2_PLACEMENT_3D('',#6853,#4285,#4286);
#3552=AXIS2_PLACEMENT_3D('',#6888,#4289,#4290);
#3553=AXIS2_PLACEMENT_3D('',#6890,#4291,#4292);
#3554=AXIS2_PLACEMENT_3D('',#6902,#4294,#4295);
#3555=AXIS2_PLACEMENT_3D('',#6903,#4296,#4297);
#3556=AXIS2_PLACEMENT_3D('',#6904,#4298,#4299);
#3557=AXIS2_PLACEMENT_3D('',#6905,#4300,#4301);
#3558=AXIS2_PLACEMENT_3D('',#6906,#4302,#4303);
#3559=AXIS2_PLACEMENT_3D('',#6907,#4304,#4305);
#3560=AXIS2_PLACEMENT_3D('',#6908,#4306,#4307);
#3561=AXIS2_PLACEMENT_3D('',#6909,#4308,#4309);
#3562=AXIS2_PLACEMENT_3D('',#6910,#4310,#4311);
#3563=AXIS2_PLACEMENT_3D('',#6911,#4312,#4313);
#3564=AXIS2_PLACEMENT_3D('',#6912,#4314,#4315);
#3565=AXIS2_PLACEMENT_3D('',#6913,#4316,#4317);
#3566=AXIS2_PLACEMENT_3D('',#6914,#4318,#4319);
#3567=AXIS2_PLACEMENT_3D('',#6915,#4320,#4321);
#3568=AXIS2_PLACEMENT_3D('',#6916,#4322,#4323);
#3569=AXIS2_PLACEMENT_3D('',#6917,#4324,#4325);
#3570=AXIS2_PLACEMENT_3D('',#6918,#4326,#4327);
#3571=AXIS2_PLACEMENT_3D('',#6919,#4328,#4329);
#3572=AXIS2_PLACEMENT_3D('',#6920,#4330,#4331);
#3573=AXIS2_PLACEMENT_3D('',#6921,#4332,#4333);
#3574=AXIS2_PLACEMENT_3D('',#6922,#4334,#4335);
#3575=AXIS2_PLACEMENT_3D('',#6923,#4336,#4337);
#3576=AXIS2_PLACEMENT_3D('',#6924,#4338,#4339);
#3577=AXIS2_PLACEMENT_3D('',#6925,#4340,#4341);
#3578=AXIS2_PLACEMENT_3D('',#6927,#4342,#4343);
#3579=AXIS2_PLACEMENT_3D('',#6936,#4344,#4345);
#3580=AXIS2_PLACEMENT_3D('',#6938,#4346,#4347);
#3581=AXIS2_PLACEMENT_3D('',#6940,#4349,#4350);
#3582=AXIS2_PLACEMENT_3D('',#6943,#4352,#4353);
#3583=AXIS2_PLACEMENT_3D('',#6944,#4354,#4355);
#3584=AXIS2_PLACEMENT_3D('',#6945,#4356,#4357);
#3585=AXIS2_PLACEMENT_3D('',#6946,#4358,#4359);
#3586=AXIS2_PLACEMENT_3D('',#6947,#4360,#4361);
#3587=AXIS2_PLACEMENT_3D('',#6948,#4362,#4363);
#3588=AXIS2_PLACEMENT_3D('',#6949,#4364,#4365);
#3589=AXIS2_PLACEMENT_3D('',#6950,#4366,#4367);
#3590=AXIS2_PLACEMENT_3D('',#6951,#4368,#4369);
#3591=AXIS2_PLACEMENT_3D('',#6952,#4370,#4371);
#3592=AXIS2_PLACEMENT_3D('',#6953,#4372,#4373);
#3593=AXIS2_PLACEMENT_3D('',#6954,#4374,#4375);
#3594=AXIS2_PLACEMENT_3D('',#6955,#4376,#4377);
#3595=AXIS2_PLACEMENT_3D('',#6956,#4378,#4379);
#3596=AXIS2_PLACEMENT_3D('',#6957,#4380,#4381);
#3597=AXIS2_PLACEMENT_3D('',#6958,#4382,#4383);
#3598=AXIS2_PLACEMENT_3D('',#6959,#4384,#4385);
#3599=AXIS2_PLACEMENT_3D('',#6960,#4386,#4387);
#3600=AXIS2_PLACEMENT_3D('',#6961,#4388,#4389);
#3601=AXIS2_PLACEMENT_3D('',#6962,#4390,#4391);
#3602=AXIS2_PLACEMENT_3D('',#6963,#4392,#4393);
#3603=AXIS2_PLACEMENT_3D('',#6964,#4394,#4395);
#3604=AXIS2_PLACEMENT_3D('',#6965,#4396,#4397);
#3605=AXIS2_PLACEMENT_3D('',#6966,#4398,#4399);
#3606=AXIS2_PLACEMENT_3D('',#6967,#4400,#4401);
#3607=AXIS2_PLACEMENT_3D('',#6968,#4402,#4403);
#3608=AXIS2_PLACEMENT_3D('',#6969,#4404,#4405);
#3609=AXIS2_PLACEMENT_3D('',#6970,#4406,#4407);
#3610=AXIS2_PLACEMENT_3D('',#6971,#4408,#4409);
#3611=AXIS2_PLACEMENT_3D('',#6972,#4410,#4411);
#3612=AXIS2_PLACEMENT_3D('',#6973,#4412,#4413);
#3613=AXIS2_PLACEMENT_3D('',#6974,#4414,#4415);
#3614=AXIS2_PLACEMENT_3D('',#6975,#4416,#4417);
#3615=AXIS2_PLACEMENT_3D('',#6976,#4418,#4419);
#3616=AXIS2_PLACEMENT_3D('',#6977,#4420,#4421);
#3617=AXIS2_PLACEMENT_3D('',#6978,#4422,#4423);
#3618=AXIS2_PLACEMENT_3D('',#6979,#4424,#4425);
#3619=AXIS2_PLACEMENT_3D('',#6980,#4426,#4427);
#3620=AXIS2_PLACEMENT_3D('',#6981,#4428,#4429);
#3621=AXIS2_PLACEMENT_3D('',#6982,#4430,#4431);
#3622=AXIS2_PLACEMENT_3D('',#6983,#4432,#4433);
#3623=AXIS2_PLACEMENT_3D('',#6984,#4434,#4435);
#3624=AXIS2_PLACEMENT_3D('',#6985,#4436,#4437);
#3625=AXIS2_PLACEMENT_3D('',#6986,#4438,#4439);
#3626=AXIS2_PLACEMENT_3D('',#6987,#4440,#4441);
#3627=AXIS2_PLACEMENT_3D('',#6988,#4442,#4443);
#3628=AXIS2_PLACEMENT_3D('',#7006,#4444,#4445);
#3629=AXIS2_PLACEMENT_3D('',#7008,#4446,#4447);
#3630=AXIS2_PLACEMENT_3D('',#7010,#4449,#4450);
#3631=AXIS2_PLACEMENT_3D('',#7011,#4451,#4452);
#3632=AXIS2_PLACEMENT_3D('',#7013,#4453,#4454);
#3633=AXIS2_PLACEMENT_3D('',#7014,#4455,#4456);
#3634=AXIS2_PLACEMENT_3D('',#7016,#4457,#4458);
#3635=AXIS2_PLACEMENT_3D('',#7018,#4460,#4461);
#3636=AXIS2_PLACEMENT_3D('',#7019,#4462,#4463);
#3637=AXIS2_PLACEMENT_3D('',#7021,#4465,#4466);
#4191=DIRECTION('axis',(0.,0.,1.));
#4192=DIRECTION('refdir',(1.,0.,0.));
#4193=DIRECTION('center_axis',(-1.,0.,0.));
#4194=DIRECTION('ref_axis',(0.,0.968583161128631,-0.248689887164855));
#4195=DIRECTION('',(-1.,0.,0.));
#4196=DIRECTION('',(1.,0.,0.));
#4197=DIRECTION('center_axis',(-1.,0.,0.));
#4198=DIRECTION('ref_axis',(0.,0.876306680043864,-0.481753674101715));
#4199=DIRECTION('',(-1.,0.,0.));
#4200=DIRECTION('',(1.,0.,0.));
#4201=DIRECTION('center_axis',(-1.,0.,0.));
#4202=DIRECTION('ref_axis',(0.,0.728968627421412,-0.684547105928688));
#4203=DIRECTION('',(-1.,0.,0.));
#4204=DIRECTION('',(1.,0.,0.));
#4205=DIRECTION('center_axis',(-1.,0.,0.));
#4206=DIRECTION('ref_axis',(0.,0.535826794978997,-0.844327925502015));
#4207=DIRECTION('',(-1.,0.,0.));
#4208=DIRECTION('',(1.,0.,0.));
#4209=DIRECTION('center_axis',(-1.,0.,0.));
#4210=DIRECTION('ref_axis',(0.,0.309016994374947,-0.951056516295154));
#4211=DIRECTION('',(-1.,0.,0.));
#4212=DIRECTION('',(1.,0.,0.));
#4213=DIRECTION('center_axis',(-1.,0.,0.));
#4214=DIRECTION('ref_axis',(0.,0.0627905195293137,-0.998026728428272));
#4215=DIRECTION('',(-1.,0.,0.));
#4216=DIRECTION('',(1.,0.,0.));
#4217=DIRECTION('center_axis',(-1.,0.,0.));
#4218=DIRECTION('ref_axis',(0.,-0.187381314585725,-0.982287250728689));
#4219=DIRECTION('',(-1.,0.,0.));
#4220=DIRECTION('',(1.,0.,0.));
#4221=DIRECTION('center_axis',(-1.,0.,0.));
#4222=DIRECTION('ref_axis',(0.,-0.425779291565072,-0.90482705246602));
#4223=DIRECTION('',(-1.,0.,0.));
#4224=DIRECTION('',(1.,0.,0.));
#4225=DIRECTION('center_axis',(-1.,0.,0.));
#4226=DIRECTION('ref_axis',(0.,-0.637423989748689,-0.770513242775789));
#4227=DIRECTION('',(-1.,0.,0.));
#4228=DIRECTION('',(1.,0.,0.));
#4229=DIRECTION('center_axis',(-1.,0.,0.));
#4230=DIRECTION('ref_axis',(0.,-0.809016994374947,-0.587785252292473));
#4231=DIRECTION('',(-1.,0.,0.));
#4232=DIRECTION('',(1.,0.,0.));
#4233=DIRECTION('center_axis',(-1.,0.,0.));
#4234=DIRECTION('ref_axis',(0.,-0.929776485888251,-0.368124552684678));
#4235=DIRECTION('',(-1.,0.,0.));
#4236=DIRECTION('',(1.,0.,0.));
#4237=DIRECTION('center_axis',(-1.,0.,0.));
#4238=DIRECTION('ref_axis',(0.,-0.992114701314478,-0.125333233564304));
#4239=DIRECTION('',(-1.,0.,0.));
#4240=DIRECTION('',(1.,0.,0.));
#4241=DIRECTION('center_axis',(-1.,0.,0.));
#4242=DIRECTION('ref_axis',(0.,-0.992114701314478,0.125333233564304));
#4243=DIRECTION('',(-1.,0.,0.));
#4244=DIRECTION('',(1.,0.,0.));
#4245=DIRECTION('center_axis',(-1.,0.,0.));
#4246=DIRECTION('ref_axis',(0.,-0.929776485888251,0.368124552684678));
#4247=DIRECTION('',(-1.,0.,0.));
#4248=DIRECTION('',(1.,0.,0.));
#4249=DIRECTION('center_axis',(-1.,0.,0.));
#4250=DIRECTION('ref_axis',(0.,-0.809016994374947,0.587785252292473));
#4251=DIRECTION('',(-1.,0.,0.));
#4252=DIRECTION('',(1.,0.,0.));
#4253=DIRECTION('center_axis',(-1.,0.,0.));
#4254=DIRECTION('ref_axis',(0.,-0.63742398974869,0.770513242775789));
#4255=DIRECTION('',(-1.,0.,0.));
#4256=DIRECTION('',(1.,0.,0.));
#4257=DIRECTION('center_axis',(-1.,0.,0.));
#4258=DIRECTION('ref_axis',(0.,-0.425779291565073,0.904827052466019));
#4259=DIRECTION('',(-1.,0.,0.));
#4260=DIRECTION('',(1.,0.,0.));
#4261=DIRECTION('center_axis',(-1.,0.,0.));
#4262=DIRECTION('ref_axis',(0.,-0.187381314585725,0.982287250728689));
#4263=DIRECTION('',(-1.,0.,0.));
#4264=DIRECTION('',(1.,0.,0.));
#4265=DIRECTION('center_axis',(-1.,0.,0.));
#4266=DIRECTION('ref_axis',(0.,0.0627905195293132,0.998026728428272));
#4267=DIRECTION('',(-1.,0.,0.));
#4268=DIRECTION('',(1.,0.,0.));
#4269=DIRECTION('center_axis',(-1.,0.,0.));
#4270=DIRECTION('ref_axis',(0.,0.309016994374947,0.951056516295154));
#4271=DIRECTION('',(-1.,0.,0.));
#4272=DIRECTION('',(1.,0.,0.));
#4273=DIRECTION('center_axis',(-1.,0.,0.));
#4274=DIRECTION('ref_axis',(0.,0.535826794978997,0.844327925502015));
#4275=DIRECTION('',(-1.,0.,0.));
#4276=DIRECTION('',(1.,0.,0.));
#4277=DIRECTION('center_axis',(-1.,0.,0.));
#4278=DIRECTION('ref_axis',(0.,0.728968627421412,0.684547105928689));
#4279=DIRECTION('',(-1.,0.,0.));
#4280=DIRECTION('',(1.,0.,0.));
#4281=DIRECTION('center_axis',(-1.,0.,0.));
#4282=DIRECTION('ref_axis',(0.,0.876306680043864,0.481753674101715));
#4283=DIRECTION('',(-1.,0.,0.));
#4284=DIRECTION('',(1.,0.,0.));
#4285=DIRECTION('center_axis',(-1.,0.,0.));
#4286=DIRECTION('ref_axis',(0.,0.968583161128631,0.248689887164855));
#4287=DIRECTION('',(-1.,0.,0.));
#4288=DIRECTION('',(1.,0.,0.));
#4289=DIRECTION('center_axis',(-1.,0.,0.));
#4290=DIRECTION('ref_axis',(0.,0.,-1.));
#4291=DIRECTION('center_axis',(1.,0.,0.));
#4292=DIRECTION('ref_axis',(0.,0.,-1.));
#4293=DIRECTION('',(-0.705535732530397,-8.67875770714651E-17,0.708674347018993));
#4294=DIRECTION('center_axis',(1.,0.,0.));
#4295=DIRECTION('ref_axis',(0.,0.,-1.));
#4296=DIRECTION('center_axis',(1.,0.,0.));
#4297=DIRECTION('ref_axis',(0.,0.,-1.));
#4298=DIRECTION('center_axis',(1.,0.,0.));
#4299=DIRECTION('ref_axis',(0.,0.,-1.));
#4300=DIRECTION('center_axis',(1.,0.,0.));
#4301=DIRECTION('ref_axis',(0.,0.,-1.));
#4302=DIRECTION('center_axis',(1.,0.,0.));
#4303=DIRECTION('ref_axis',(0.,0.,-1.));
#4304=DIRECTION('center_axis',(1.,0.,0.));
#4305=DIRECTION('ref_axis',(0.,0.,-1.));
#4306=DIRECTION('center_axis',(1.,0.,0.));
#4307=DIRECTION('ref_axis',(0.,0.,-1.));
#4308=DIRECTION('center_axis',(1.,0.,0.));
#4309=DIRECTION('ref_axis',(0.,0.,-1.));
#4310=DIRECTION('center_axis',(1.,0.,0.));
#4311=DIRECTION('ref_axis',(0.,0.,-1.));
#4312=DIRECTION('center_axis',(1.,0.,0.));
#4313=DIRECTION('ref_axis',(0.,0.,-1.));
#4314=DIRECTION('center_axis',(1.,0.,0.));
#4315=DIRECTION('ref_axis',(0.,0.,-1.));
#4316=DIRECTION('center_axis',(1.,0.,0.));
#4317=DIRECTION('ref_axis',(0.,0.,-1.));
#4318=DIRECTION('center_axis',(1.,0.,0.));
#4319=DIRECTION('ref_axis',(0.,0.,-1.));
#4320=DIRECTION('center_axis',(1.,0.,0.));
#4321=DIRECTION('ref_axis',(0.,0.,-1.));
#4322=DIRECTION('center_axis',(1.,0.,0.));
#4323=DIRECTION('ref_axis',(0.,0.,-1.));
#4324=DIRECTION('center_axis',(1.,0.,0.));
#4325=DIRECTION('ref_axis',(0.,0.,-1.));
#4326=DIRECTION('center_axis',(1.,0.,0.));
#4327=DIRECTION('ref_axis',(0.,0.,-1.));
#4328=DIRECTION('center_axis',(1.,0.,0.));
#4329=DIRECTION('ref_axis',(0.,0.,-1.));
#4330=DIRECTION('center_axis',(1.,0.,0.));
#4331=DIRECTION('ref_axis',(0.,0.,-1.));
#4332=DIRECTION('center_axis',(1.,0.,0.));
#4333=DIRECTION('ref_axis',(0.,0.,-1.));
#4334=DIRECTION('center_axis',(1.,0.,0.));
#4335=DIRECTION('ref_axis',(0.,0.,-1.));
#4336=DIRECTION('center_axis',(1.,0.,0.));
#4337=DIRECTION('ref_axis',(0.,0.,-1.));
#4338=DIRECTION('center_axis',(1.,0.,0.));
#4339=DIRECTION('ref_axis',(0.,0.,-1.));
#4340=DIRECTION('center_axis',(1.,0.,0.));
#4341=DIRECTION('ref_axis',(0.,0.,-1.));
#4342=DIRECTION('center_axis',(1.,0.,0.));
#4343=DIRECTION('ref_axis',(0.,0.,-1.));
#4344=DIRECTION('center_axis',(1.,0.,0.));
#4345=DIRECTION('ref_axis',(0.,0.,-1.));
#4346=DIRECTION('center_axis',(1.,0.,0.));
#4347=DIRECTION('ref_axis',(0.,0.,-1.));
#4348=DIRECTION('',(1.,0.,0.));
#4349=DIRECTION('center_axis',(1.,0.,0.));
#4350=DIRECTION('ref_axis',(0.,0.,-1.));
#4351=DIRECTION('',(-1.,0.,0.));
#4352=DIRECTION('center_axis',(1.,0.,0.));
#4353=DIRECTION('ref_axis',(0.,0.,-1.));
#4354=DIRECTION('center_axis',(1.,0.,0.));
#4355=DIRECTION('ref_axis',(0.,0.,-1.));
#4356=DIRECTION('center_axis',(1.,0.,0.));
#4357=DIRECTION('ref_axis',(0.,0.,-1.));
#4358=DIRECTION('center_axis',(1.,0.,0.));
#4359=DIRECTION('ref_axis',(0.,0.,-1.));
#4360=DIRECTION('center_axis',(1.,0.,0.));
#4361=DIRECTION('ref_axis',(0.,0.,-1.));
#4362=DIRECTION('center_axis',(1.,0.,0.));
#4363=DIRECTION('ref_axis',(0.,0.,-1.));
#4364=DIRECTION('center_axis',(1.,0.,0.));
#4365=DIRECTION('ref_axis',(0.,0.,-1.));
#4366=DIRECTION('center_axis',(1.,0.,0.));
#4367=DIRECTION('ref_axis',(0.,0.,-1.));
#4368=DIRECTION('center_axis',(1.,0.,0.));
#4369=DIRECTION('ref_axis',(0.,0.,-1.));
#4370=DIRECTION('center_axis',(1.,0.,0.));
#4371=DIRECTION('ref_axis',(0.,0.,-1.));
#4372=DIRECTION('center_axis',(1.,0.,0.));
#4373=DIRECTION('ref_axis',(0.,0.,-1.));
#4374=DIRECTION('center_axis',(1.,0.,0.));
#4375=DIRECTION('ref_axis',(0.,0.,-1.));
#4376=DIRECTION('center_axis',(1.,0.,0.));
#4377=DIRECTION('ref_axis',(0.,0.,-1.));
#4378=DIRECTION('center_axis',(1.,0.,0.));
#4379=DIRECTION('ref_axis',(0.,0.,-1.));
#4380=DIRECTION('center_axis',(1.,0.,0.));
#4381=DIRECTION('ref_axis',(0.,0.,-1.));
#4382=DIRECTION('center_axis',(1.,0.,0.));
#4383=DIRECTION('ref_axis',(0.,0.,-1.));
#4384=DIRECTION('center_axis',(1.,0.,0.));
#4385=DIRECTION('ref_axis',(0.,0.,-1.));
#4386=DIRECTION('center_axis',(1.,0.,0.));
#4387=DIRECTION('ref_axis',(0.,0.,-1.));
#4388=DIRECTION('center_axis',(1.,0.,0.));
#4389=DIRECTION('ref_axis',(0.,0.,-1.));
#4390=DIRECTION('center_axis',(1.,0.,0.));
#4391=DIRECTION('ref_axis',(0.,0.,-1.));
#4392=DIRECTION('center_axis',(1.,0.,0.));
#4393=DIRECTION('ref_axis',(0.,0.,-1.));
#4394=DIRECTION('center_axis',(1.,0.,0.));
#4395=DIRECTION('ref_axis',(0.,0.,-1.));
#4396=DIRECTION('center_axis',(1.,0.,0.));
#4397=DIRECTION('ref_axis',(0.,0.,-1.));
#4398=DIRECTION('center_axis',(1.,0.,0.));
#4399=DIRECTION('ref_axis',(0.,0.,-1.));
#4400=DIRECTION('center_axis',(1.,0.,0.));
#4401=DIRECTION('ref_axis',(0.,0.,-1.));
#4402=DIRECTION('center_axis',(1.,0.,0.));
#4403=DIRECTION('ref_axis',(0.,0.,-1.));
#4404=DIRECTION('center_axis',(1.,0.,0.));
#4405=DIRECTION('ref_axis',(0.,0.,-1.));
#4406=DIRECTION('center_axis',(1.,0.,0.));
#4407=DIRECTION('ref_axis',(0.,0.,-1.));
#4408=DIRECTION('center_axis',(1.,0.,0.));
#4409=DIRECTION('ref_axis',(0.,0.,-1.));
#4410=DIRECTION('center_axis',(1.,0.,0.));
#4411=DIRECTION('ref_axis',(0.,0.,-1.));
#4412=DIRECTION('center_axis',(1.,0.,0.));
#4413=DIRECTION('ref_axis',(0.,0.,-1.));
#4414=DIRECTION('center_axis',(1.,0.,0.));
#4415=DIRECTION('ref_axis',(0.,0.,-1.));
#4416=DIRECTION('center_axis',(1.,0.,0.));
#4417=DIRECTION('ref_axis',(0.,0.,-1.));
#4418=DIRECTION('center_axis',(1.,0.,0.));
#4419=DIRECTION('ref_axis',(0.,0.,-1.));
#4420=DIRECTION('center_axis',(1.,0.,0.));
#4421=DIRECTION('ref_axis',(0.,0.,-1.));
#4422=DIRECTION('center_axis',(1.,0.,0.));
#4423=DIRECTION('ref_axis',(0.,0.,-1.));
#4424=DIRECTION('center_axis',(1.,0.,0.));
#4425=DIRECTION('ref_axis',(0.,0.,-1.));
#4426=DIRECTION('center_axis',(1.,0.,0.));
#4427=DIRECTION('ref_axis',(0.,0.,-1.));
#4428=DIRECTION('center_axis',(1.,0.,0.));
#4429=DIRECTION('ref_axis',(0.,0.,-1.));
#4430=DIRECTION('center_axis',(1.,0.,0.));
#4431=DIRECTION('ref_axis',(0.,0.,-1.));
#4432=DIRECTION('center_axis',(1.,0.,0.));
#4433=DIRECTION('ref_axis',(0.,0.,-1.));
#4434=DIRECTION('center_axis',(1.,0.,0.));
#4435=DIRECTION('ref_axis',(0.,0.,-1.));
#4436=DIRECTION('center_axis',(1.,0.,0.));
#4437=DIRECTION('ref_axis',(0.,0.,-1.));
#4438=DIRECTION('center_axis',(1.,0.,0.));
#4439=DIRECTION('ref_axis',(0.,0.,-1.));
#4440=DIRECTION('center_axis',(1.,0.,0.));
#4441=DIRECTION('ref_axis',(0.,0.,-1.));
#4442=DIRECTION('center_axis',(-1.,0.,0.));
#4443=DIRECTION('ref_axis',(0.,1.,0.));
#4444=DIRECTION('center_axis',(1.,0.,0.));
#4445=DIRECTION('ref_axis',(0.,0.,-1.));
#4446=DIRECTION('center_axis',(1.,0.,0.));
#4447=DIRECTION('ref_axis',(0.,0.,-1.));
#4448=DIRECTION('',(-1.,0.,0.));
#4449=DIRECTION('center_axis',(1.,0.,0.));
#4450=DIRECTION('ref_axis',(0.,0.,-1.));
#4451=DIRECTION('center_axis',(-1.,0.,0.));
#4452=DIRECTION('ref_axis',(0.,0.,1.));
#4453=DIRECTION('center_axis',(1.,0.,0.));
#4454=DIRECTION('ref_axis',(0.,0.,-1.));
#4455=DIRECTION('center_axis',(1.,0.,0.));
#4456=DIRECTION('ref_axis',(0.,0.,-1.));
#4457=DIRECTION('center_axis',(1.,0.,0.));
#4458=DIRECTION('ref_axis',(0.,0.,-1.));
#4459=DIRECTION('',(-1.,0.,0.));
#4460=DIRECTION('center_axis',(1.,0.,0.));
#4461=DIRECTION('ref_axis',(0.,0.,-1.));
#4462=DIRECTION('center_axis',(1.,0.,0.));
#4463=DIRECTION('ref_axis',(0.,0.,-1.));
#4464=DIRECTION('',(-0.708674347018993,8.64032076527434E-17,-0.705535732530397));
#4465=DIRECTION('center_axis',(1.,0.,0.));
#4466=DIRECTION('ref_axis',(0.,0.,-1.));
#6047=CARTESIAN_POINT('',(0.,0.,0.));
#6048=CARTESIAN_POINT('Origin',(65.0333054217745,2.89627205572787,11.2802348949791));
#6049=CARTESIAN_POINT('',(40.4874595913632,1.99731386475336,10.8422004546896));
#6050=CARTESIAN_POINT('',(40.4874595913632,3.47301042256638,10.4633059774983));
#6051=CARTESIAN_POINT('Ctrl Pts',(40.4874595913632,1.99731386475335,10.8422004546896));
#6052=CARTESIAN_POINT('Ctrl Pts',(40.4362950734394,2.02504082610839,10.7852976709622));
#6053=CARTESIAN_POINT('Ctrl Pts',(40.3883369165899,2.05851119287108,10.7303891684628));
#6054=CARTESIAN_POINT('Ctrl Pts',(40.2799612282044,2.15565705872171,10.601352159818));
#6055=CARTESIAN_POINT('Ctrl Pts',(40.2177890646542,2.2340948035392,10.5221252828469));
#6056=CARTESIAN_POINT('Ctrl Pts',(40.1312057824654,2.42334768794107,10.391667759134));
#6057=CARTESIAN_POINT('Ctrl Pts',(40.107260046221,2.53453990097136,10.3406760550451));
#6058=CARTESIAN_POINT('Ctrl Pts',(40.107260046221,2.76062443615468,10.282627412656));
#6059=CARTESIAN_POINT('Ctrl Pts',(40.1312057824654,2.88262835599554,10.2737445264171));
#6060=CARTESIAN_POINT('Ctrl Pts',(40.2177890646542,3.11132031417736,10.2968920535137));
#6061=CARTESIAN_POINT('Ctrl Pts',(40.2799612282044,3.21822367299693,10.3285314232885));
#6062=CARTESIAN_POINT('Ctrl Pts',(40.3883369165899,3.3655172971902,10.3948070381394));
#6063=CARTESIAN_POINT('Ctrl Pts',(40.4362950734393,3.42129997598637,10.4267992535094));
#6064=CARTESIAN_POINT('Ctrl Pts',(40.4874595913632,3.47301042256638,10.4633059774983));
#6065=CARTESIAN_POINT('',(44.4440437425414,1.99731386475336,10.8422004546896));
#6066=CARTESIAN_POINT('',(65.0333054217745,1.99731386475335,10.8422004546896));
#6067=CARTESIAN_POINT('',(44.4440437425414,3.47301042256638,10.4633059774983));
#6068=CARTESIAN_POINT('Ctrl Pts',(44.4440437425414,3.47301042256638,10.4633059774983));
#6069=CARTESIAN_POINT('Ctrl Pts',(44.494558600482,3.42150132578768,10.4269414031543));
#6070=CARTESIAN_POINT('Ctrl Pts',(44.5419028922086,3.36596803166599,10.3950689245517));
#6071=CARTESIAN_POINT('Ctrl Pts',(44.6493790253187,3.21879552819819,10.3287004100455));
#6072=CARTESIAN_POINT('Ctrl Pts',(44.7111607127654,3.11169821280053,10.2969577118196));
#6073=CARTESIAN_POINT('Ctrl Pts',(44.7971423090715,2.8827215071592,10.2737266025933));
#6074=CARTESIAN_POINT('Ctrl Pts',(44.8208830494268,2.76063081774635,10.2826257741417));
#6075=CARTESIAN_POINT('Ctrl Pts',(44.8208830494268,2.53453351937968,10.3406776935593));
#6076=CARTESIAN_POINT('Ctrl Pts',(44.7971423090715,2.42325742408613,10.3916969282828));
#6077=CARTESIAN_POINT('Ctrl Pts',(44.7111607127654,2.23379527958143,10.5223648737091));
#6078=CARTESIAN_POINT('Ctrl Pts',(44.6493790253187,2.15523734817991,10.6017757373863));
#6079=CARTESIAN_POINT('Ctrl Pts',(44.5419028922086,2.05824237598036,10.7308358042651));
#6080=CARTESIAN_POINT('Ctrl Pts',(44.494558600482,2.0249328630462,10.7855192386522));
#6081=CARTESIAN_POINT('Ctrl Pts',(44.4440437425414,1.99731386475335,10.8422004546895));
#6082=CARTESIAN_POINT('',(65.0333054217745,3.47301042256639,10.4633059774983));
#6083=CARTESIAN_POINT('Origin',(65.0333054217745,5.61056068645085,10.2055720021147));
#6084=CARTESIAN_POINT('',(40.4874595913632,4.63091018458434,10.0048610303352));
#6085=CARTESIAN_POINT('',(40.4874595913632,5.96601779663743,9.270879409431));
#6086=CARTESIAN_POINT('Ctrl Pts',(40.4874595913632,4.63091018458433,10.0048610303352));
#6087=CARTESIAN_POINT('Ctrl Pts',(40.4362950734394,4.64361490559755,9.94285053730468));
#6088=CARTESIAN_POINT('Ctrl Pts',(40.3883369165899,4.66237854994973,9.88134334464741));
#6089=CARTESIAN_POINT('Ctrl Pts',(40.2799612282044,4.72438220066596,9.73220107649475));
#6090=CARTESIAN_POINT('Ctrl Pts',(40.2177890646542,4.78065275639872,9.63595658364359));
#6091=CARTESIAN_POINT('Ctrl Pts',(40.1312057824654,4.93151644657343,9.46253234446524));
#6092=CARTESIAN_POINT('Ctrl Pts',(40.107260046221,5.02653423062696,9.38549025961531));
#6093=CARTESIAN_POINT('Ctrl Pts',(40.107260046221,5.2310797940713,9.27304038452639));
#6094=CARTESIAN_POINT('Ctrl Pts',(40.1312057824654,5.34704165244441,9.23409542943431));
#6095=CARTESIAN_POINT('Ctrl Pts',(40.2177890646542,5.57430538812665,9.19964235712613));
#6096=CARTESIAN_POINT('Ctrl Pts',(40.2799612282044,5.68571857264663,9.20370193367626));
#6097=CARTESIAN_POINT('Ctrl Pts',(40.3883369165899,5.84486677196091,9.23126494343362));
#6098=CARTESIAN_POINT('Ctrl Pts',(40.4362950734394,5.90685307575603,9.24837947643258));
#6099=CARTESIAN_POINT('Ctrl Pts',(40.4874595913632,5.96601779663743,9.270879409431));
#6100=CARTESIAN_POINT('',(44.4440437425414,4.63091018458434,10.0048610303352));
#6101=CARTESIAN_POINT('',(65.0333054217746,4.63091018458433,10.0048610303352));
#6102=CARTESIAN_POINT('',(44.4440437425414,5.96601779663743,9.270879409431));
#6103=CARTESIAN_POINT('Ctrl Pts',(44.4440437425414,5.96601779663743,9.270879409431));
#6104=CARTESIAN_POINT('Ctrl Pts',(44.494558600482,5.90708345096223,9.24846708652567));
#6105=CARTESIAN_POINT('Ctrl Pts',(44.5419028922086,5.84536847428662,9.2314065090968));
#6106=CARTESIAN_POINT('Ctrl Pts',(44.6493790253187,5.68631448726271,9.20372339679809));
#6107=CARTESIAN_POINT('Ctrl Pts',(44.7111607127654,5.57468774292636,9.19961197308963));
#6108=CARTESIAN_POINT('Ctrl Pts',(44.7971423090715,5.34712741961925,9.23405490296801));
#6109=CARTESIAN_POINT('Ctrl Pts',(44.8208830494268,5.23108556769161,9.27303721045176));
#6110=CARTESIAN_POINT('Ctrl Pts',(44.8208830494268,5.02652845700665,9.38549343368993));
#6111=CARTESIAN_POINT('Ctrl Pts',(44.7971423090715,4.93143627259579,9.4625830449195));
#6112=CARTESIAN_POINT('Ctrl Pts',(44.7111607127654,4.78042222636135,9.63626313589754));
#6113=CARTESIAN_POINT('Ctrl Pts',(44.6493790253187,4.72408101556028,9.7327157243621));
#6114=CARTESIAN_POINT('Ctrl Pts',(44.5419028922086,4.66222925224323,9.88184280060689));
#6115=CARTESIAN_POINT('Ctrl Pts',(44.494558600482,4.64356543603732,9.94309199336003));
#6116=CARTESIAN_POINT('Ctrl Pts',(44.4440437425414,4.63091018458433,10.0048610303352));
#6117=CARTESIAN_POINT('',(65.0333054217746,5.96601779663744,9.270879409431));
#6118=CARTESIAN_POINT('Origin',(65.0333054217745,7.97231715504529,8.48965548688909));
#6119=CARTESIAN_POINT('',(40.4874595913632,6.97352938622157,8.53887939213984));
#6120=CARTESIAN_POINT('',(40.4874595913632,8.08415833106712,7.49592939215974));
#6121=CARTESIAN_POINT('Ctrl Pts',(40.4874595913632,6.97352938622157,8.53887939213984));
#6122=CARTESIAN_POINT('Ctrl Pts',(40.4362950734394,6.97041358254702,8.47565753714199));
#6123=CARTESIAN_POINT('Ctrl Pts',(40.3883369165899,6.97329151570619,8.41141637744912));
#6124=CARTESIAN_POINT('Ctrl Pts',(40.2799612282044,6.99625703388003,8.25154000700349));
#6125=CARTESIAN_POINT('Ctrl Pts',(40.2177890646542,7.02682471456273,8.14432529372061));
#6126=CARTESIAN_POINT('Ctrl Pts',(40.1312057824654,7.12981989001876,7.93883122183409));
#6127=CARTESIAN_POINT('Ctrl Pts',(40.107260046221,7.2026929282725,7.84057959375527));
#6128=CARTESIAN_POINT('Ctrl Pts',(40.107260046221,7.37284716996069,7.68079412518009));
#6129=CARTESIAN_POINT('Ctrl Pts',(40.1312057824654,7.47548065682658,7.61423415599275));
#6130=CARTESIAN_POINT('Ctrl Pts',(40.2177890646542,7.68703635367878,7.52434529752242));
#6131=CARTESIAN_POINT('Ctrl Pts',(40.2799612282044,7.79595886376674,7.50057000272324));
#6132=CARTESIAN_POINT('Ctrl Pts',(40.3883369165899,7.95696177153297,7.48768852211428));
#6133=CARTESIAN_POINT('Ctrl Pts',(40.4362950734394,8.02125687288992,7.48885000369109));
#6134=CARTESIAN_POINT('Ctrl Pts',(40.4874595913632,8.08415833106712,7.49592939215974));
#6135=CARTESIAN_POINT('',(44.4440437425414,6.97352938622157,8.53887939213984));
#6136=CARTESIAN_POINT('',(65.0333054217745,6.97352938622157,8.53887939213985));
#6137=CARTESIAN_POINT('',(44.4440437425414,8.08415833106712,7.49592939215974));
#6138=CARTESIAN_POINT('Ctrl Pts',(44.4440437425414,8.08415833106712,7.49592939215974));
#6139=CARTESIAN_POINT('Ctrl Pts',(44.494558600482,8.02150179817957,7.48887756936796));
#6140=CARTESIAN_POINT('Ctrl Pts',(44.5419028922086,7.95748291790636,7.48770087193706));
#6141=CARTESIAN_POINT('Ctrl Pts',(44.6493790253187,7.79654139429069,7.500442593603));
#6142=CARTESIAN_POINT('Ctrl Pts',(44.7111607127654,7.68739913989674,7.52422078028431));
#6143=CARTESIAN_POINT('Ctrl Pts',(44.7971423090715,7.47555365094558,7.61417357331088));
#6144=CARTESIAN_POINT('Ctrl Pts',(44.8208830494268,7.37285197283185,7.68078961498387));
#6145=CARTESIAN_POINT('Ctrl Pts',(44.8208830494268,7.20268812540135,7.8405841039515));
#6146=CARTESIAN_POINT('Ctrl Pts',(44.7971423090715,7.12975484354432,7.9389002678978));
#6147=CARTESIAN_POINT('Ctrl Pts',(44.7111607127654,7.02667766349585,8.14467954556077));
#6148=CARTESIAN_POINT('Ctrl Pts',(44.6493790253187,6.99609329877835,8.25211338795166));
#6149=CARTESIAN_POINT('Ctrl Pts',(44.5419028922086,6.97327111810788,8.41193727091097));
#6150=CARTESIAN_POINT('Ctrl Pts',(44.494558600482,6.97042571484315,8.47590370999069));
#6151=CARTESIAN_POINT('Ctrl Pts',(44.4440437425414,6.97352938622157,8.53887939213984));
#6152=CARTESIAN_POINT('',(65.0333054217745,8.08415833106713,7.49592939215974));
#6153=CARTESIAN_POINT('Origin',(65.0333054217745,9.83314361665672,6.24030269465341));
#6154=CARTESIAN_POINT('',(40.4874595913632,8.87797608967546,6.53636855793469));
#6155=CARTESIAN_POINT('',(40.4874595913632,9.69434146610128,5.2499825630792));
#6156=CARTESIAN_POINT('Ctrl Pts',(40.4874595913632,8.87797608967545,6.53636855793469));
#6157=CARTESIAN_POINT('Ctrl Pts',(40.4362950734394,8.85923553871713,6.47590780263271));
#6158=CARTESIAN_POINT('Ctrl Pts',(40.3883369165899,8.84604692955859,6.41296918423019));
#6159=CARTESIAN_POINT('Ctrl Pts',(40.2799612282044,8.82853130722192,6.25240433183086));
#6160=CARTESIAN_POINT('Ctrl Pts',(40.2177890646542,8.83147543305721,6.14095609285996));
#6161=CARTESIAN_POINT('Ctrl Pts',(40.1312057824654,8.88013052813091,5.91630413655623));
#6162=CARTESIAN_POINT('Ctrl Pts',(40.107260046221,8.92627993958308,5.80301647638493));
#6163=CARTESIAN_POINT('Ctrl Pts',(40.107260046221,9.05135144272633,5.6059353229639));
#6164=CARTESIAN_POINT('Ctrl Pts',(40.1312057824654,9.13420771864564,5.51594254733579));
#6165=CARTESIAN_POINT('Ctrl Pts',(40.2177890646542,9.31676255418716,5.3762659502691));
#6166=CARTESIAN_POINT('Ctrl Pts',(40.2799612282044,9.4163503879453,5.32614967333226));
#6167=CARTESIAN_POINT('Ctrl Pts',(40.3883369165899,9.56909159934126,5.27363309315842));
#6168=CARTESIAN_POINT('Ctrl Pts',(40.4362950734394,9.63165560058094,5.25876854315396));
#6169=CARTESIAN_POINT('Ctrl Pts',(40.4874595913632,9.69434146610128,5.24998256307919));
#6170=CARTESIAN_POINT('',(44.4440437425414,8.87797608967546,6.53636855793469));
#6171=CARTESIAN_POINT('',(65.0333054217745,8.87797608967545,6.5363685579347));
#6172=CARTESIAN_POINT('',(44.4440437425414,9.69434146610128,5.2499825630792));
#6173=CARTESIAN_POINT('Ctrl Pts',(44.4440437425414,9.69434146610128,5.24998256307919));
#6174=CARTESIAN_POINT('Ctrl Pts',(44.494558600482,9.6318996863973,5.25873433236176));
#6175=CARTESIAN_POINT('Ctrl Pts',(44.5419028922086,9.56959944421904,5.27351545115601));
#6176=CARTESIAN_POINT('Ctrl Pts',(44.6493790253187,9.4168829318419,5.32588139755355));
#6177=CARTESIAN_POINT('Ctrl Pts',(44.7111607127654,9.31708297663106,5.37605512370539));
#6178=CARTESIAN_POINT('Ctrl Pts',(44.7971423090715,9.13426335321984,5.51586571507106));
#6179=CARTESIAN_POINT('Ctrl Pts',(44.8208830494268,9.05135497306626,5.6059297600383));
#6180=CARTESIAN_POINT('Ctrl Pts',(44.8208830494268,8.92627640924314,5.80302203931053));
#6181=CARTESIAN_POINT('Ctrl Pts',(44.7971423090715,8.88008469626887,5.91638718981127));
#6182=CARTESIAN_POINT('Ctrl Pts',(44.7111607127654,8.83142110072016,6.14133578534036));
#6183=CARTESIAN_POINT('Ctrl Pts',(44.6493790253187,8.82851531020285,6.25300041822613));
#6184=CARTESIAN_POINT('Ctrl Pts',(44.5419028922086,8.8461567137246,6.41347878554251));
#6185=CARTESIAN_POINT('Ctrl Pts',(44.494558600482,8.85930851055284,6.47614322432933));
#6186=CARTESIAN_POINT('Ctrl Pts',(44.4440437425414,8.87797608967545,6.53636855793469));
#6187=CARTESIAN_POINT('',(65.0333054217745,9.69434146610128,5.24998256307919));
#6188=CARTESIAN_POINT('Origin',(65.0333054217745,11.0761175010611,3.59884873388474));
#6189=CARTESIAN_POINT('',(40.4874595913632,10.2245869045029,4.1231536481525));
#6190=CARTESIAN_POINT('',(40.4874595913632,10.6953934735264,2.67416002147514));
#6191=CARTESIAN_POINT('Ctrl Pts',(40.4874595913632,10.2245869045029,4.12315364815251));
#6192=CARTESIAN_POINT('Ctrl Pts',(40.4362950734394,10.1913991440005,4.06925296416111));
#6193=CARTESIAN_POINT('Ctrl Pts',(40.3883369165899,10.162972681342,4.01157155191524));
#6194=CARTESIAN_POINT('Ctrl Pts',(40.2799612282044,10.1060764894642,3.86040709775467));
#6195=CARTESIAN_POINT('Ctrl Pts',(40.2177890646542,10.0812120701981,3.75172803582823));
#6196=CARTESIAN_POINT('Ctrl Pts',(40.1312057824654,10.072469906325,3.52203390373397));
#6197=CARTESIAN_POINT('Ctrl Pts',(40.107260046221,10.0889959537284,3.40082849180162));
#6198=CARTESIAN_POINT('Ctrl Pts',(40.107260046221,10.1611260158034,3.17883498721797));
#6199=CARTESIAN_POINT('Ctrl Pts',(40.1312057824654,10.2189989162361,3.07106398221208));
#6200=CARTESIAN_POINT('Ctrl Pts',(40.2177890646542,10.3610822987601,2.89037604083731));
#6201=CARTESIAN_POINT('Ctrl Pts',(40.2799612282044,10.445077986335,2.81706777175753));
#6202=CARTESIAN_POINT('Ctrl Pts',(40.3883369165899,10.5799602093058,2.7282159018936));
#6203=CARTESIAN_POINT('Ctrl Pts',(40.4362950734394,10.636861984136,2.69825931465265));
#6204=CARTESIAN_POINT('Ctrl Pts',(40.4874595913632,10.6953934735264,2.67416002147513));
#6205=CARTESIAN_POINT('',(44.4440437425414,10.2245869045029,4.1231536481525));
#6206=CARTESIAN_POINT('',(65.0333054217745,10.2245869045029,4.12315364815251));
#6207=CARTESIAN_POINT('',(44.4440437425414,10.6953934735264,2.67416002147514));
#6208=CARTESIAN_POINT('Ctrl Pts',(44.4440437425414,10.6953934735264,2.67416002147513));
#6209=CARTESIAN_POINT('Ctrl Pts',(44.494558600482,10.6370898936696,2.69816547698127));
#6210=CARTESIAN_POINT('Ctrl Pts',(44.5419028922086,10.5804228429266,2.72797565994567));
#6211=CARTESIAN_POINT('Ctrl Pts',(44.6493790253187,10.4455270819127,2.81667548607418));
#6212=CARTESIAN_POINT('Ctrl Pts',(44.7111607127654,10.3613402241094,2.89009215195636));
#6213=CARTESIAN_POINT('Ctrl Pts',(44.7971423090715,10.2190336955406,3.07097572801825));
#6214=CARTESIAN_POINT('Ctrl Pts',(44.8208830494268,10.1611280517879,3.17882872110207));
#6215=CARTESIAN_POINT('Ctrl Pts',(44.8208830494268,10.088993917744,3.40083475791752));
#6216=CARTESIAN_POINT('Ctrl Pts',(44.7971423090715,10.0724461688598,3.52212574563888));
#6217=CARTESIAN_POINT('Ctrl Pts',(44.7111607127654,10.0812538704914,3.75210931147394));
#6218=CARTESIAN_POINT('Ctrl Pts',(44.6493790253187,10.1062092356792,3.86098843529658));
#6219=CARTESIAN_POINT('Ctrl Pts',(44.5419028922086,10.1632057491294,4.01203784095338));
#6220=CARTESIAN_POINT('Ctrl Pts',(44.494558600482,10.191528370287,4.06946284229465));
#6221=CARTESIAN_POINT('Ctrl Pts',(44.4440437425414,10.2245869045029,4.12315364815251));
#6222=CARTESIAN_POINT('',(65.0333054217745,10.6953934735264,2.67416002147513));
#6223=CARTESIAN_POINT('Origin',(65.0333054217745,11.6231381877631,0.731265871526308));
#6224=CARTESIAN_POINT('',(40.4874595913632,10.9287493207203,1.45086583075851));
#6225=CARTESIAN_POINT('',(40.4874595913632,11.0244145741041,-0.0696898291507925));
#6226=CARTESIAN_POINT('Ctrl Pts',(40.4874595913632,10.9287493207203,1.45086583075852));
#6227=CARTESIAN_POINT('Ctrl Pts',(40.4362950734394,10.8831996597221,1.40691199628575));
#6228=CARTESIAN_POINT('Ctrl Pts',(40.3883369165899,10.8413214827577,1.35811212546531));
#6229=CARTESIAN_POINT('Ctrl Pts',(40.2799612282044,10.7486197183239,1.22584628814239));
#6230=CARTESIAN_POINT('Ctrl Pts',(40.2177890646542,10.6975090768639,1.12676510841489));
#6231=CARTESIAN_POINT('Ctrl Pts',(40.1312057824654,10.6319189563517,0.906461327605495));
#6232=CARTESIAN_POINT('Ctrl Pts',(40.107260046221,10.6177832473694,0.784953945706135));
#6233=CARTESIAN_POINT('Ctrl Pts',(40.107260046221,10.6324396713002,0.551996758287852));
#6234=CARTESIAN_POINT('Ctrl Pts',(40.1312057824654,10.6616928290704,0.433219172502737));
#6235=CARTESIAN_POINT('Ctrl Pts',(40.2177890646542,10.7543771371068,0.222873174700238));
#6236=CARTESIAN_POINT('Ctrl Pts',(40.2799612282044,10.8175029205336,0.130979141632741));
#6237=CARTESIAN_POINT('Ctrl Pts',(40.3883369165899,10.9260510089478,0.0113748718365951));
#6238=CARTESIAN_POINT('Ctrl Pts',(40.4362950734394,10.9737152095859,-0.0317914700918793));
#6239=CARTESIAN_POINT('Ctrl Pts',(40.4874595913632,11.0244145741041,-0.0696898291507991));
#6240=CARTESIAN_POINT('',(44.4440437425414,10.9287493207203,1.45086583075851));
#6241=CARTESIAN_POINT('',(65.0333054217745,10.9287493207203,1.45086583075852));
#6242=CARTESIAN_POINT('',(44.4440437425414,11.0244145741041,-0.0696898291507925));
#6243=CARTESIAN_POINT('Ctrl Pts',(44.4440437425414,11.0244145741041,-0.0696898291507991));
#6244=CARTESIAN_POINT('Ctrl Pts',(44.494558600482,10.9739126224425,-0.0319390384764372));
#6245=CARTESIAN_POINT('Ctrl Pts',(44.5419028922086,10.9264393623398,0.0110271252282886));
#6246=CARTESIAN_POINT('Ctrl Pts',(44.6493790253187,10.8178403494655,0.130487494796957));
#6247=CARTESIAN_POINT('Ctrl Pts',(44.7111607127654,10.7545563589632,0.222534061284509));
#6248=CARTESIAN_POINT('Ctrl Pts',(44.7971423090715,10.6617045677936,0.43312504171538));
#6249=CARTESIAN_POINT('Ctrl Pts',(44.8208830494268,10.6324400850008,0.551990182704755));
#6250=CARTESIAN_POINT('Ctrl Pts',(44.8208830494268,10.6177828336688,0.784960521289232));
#6251=CARTESIAN_POINT('Ctrl Pts',(44.7971423090715,10.6319188047956,0.906556187395616));
#6252=CARTESIAN_POINT('Ctrl Pts',(44.7111607127654,10.6976443833215,1.12712401027484));
#6253=CARTESIAN_POINT('Ctrl Pts',(44.6493790253187,10.7488928668403,1.22637634925516));
#6254=CARTESIAN_POINT('Ctrl Pts',(44.5419028922086,10.8416631896602,1.35850580357412));
#6255=CARTESIAN_POINT('Ctrl Pts',(44.494558600482,10.8833770206965,1.40708314344118));
#6256=CARTESIAN_POINT('Ctrl Pts',(44.4440437425414,10.9287493207203,1.45086583075852));
#6257=CARTESIAN_POINT('',(65.0333054217745,11.0244145741041,-0.0696898291508022));
#6258=CARTESIAN_POINT('Origin',(65.0333054217745,11.4398343552159,-2.18226511494788));
#6259=CARTESIAN_POINT('',(40.4874595913632,10.9462182239883,-1.31258522269331));
#6260=CARTESIAN_POINT('',(40.4874595913632,10.6607311620303,-2.80916081150993));
#6261=CARTESIAN_POINT('Ctrl Pts',(40.4874595913632,10.9462182239883,-1.3125852226933));
#6262=CARTESIAN_POINT('Ctrl Pts',(40.4362950734394,10.8911687152148,-1.34383042657663));
#6263=CARTESIAN_POINT('Ctrl Pts',(40.3883369165899,10.8384701838204,-1.38068248061461));
#6264=CARTESIAN_POINT('Ctrl Pts',(40.2799612282044,10.7157876396233,-1.48573895210117));
#6265=CARTESIAN_POINT('Ctrl Pts',(40.2177890646542,10.6416422455441,-1.56899661471235));
#6266=CARTESIAN_POINT('Ctrl Pts',(40.1312057824654,10.5233254368881,-1.766067547468));
#6267=CARTESIAN_POINT('Ctrl Pts',(40.107260046221,10.479416170103,-1.88024214365675));
#6268=CARTESIAN_POINT('Ctrl Pts',(40.107260046221,10.4356780388714,-2.10952545706757));
#6269=CARTESIAN_POINT('Ctrl Pts',(40.1312057824654,10.4344733704908,-2.23184639108363));
#6270=CARTESIAN_POINT('Ctrl Pts',(40.2177890646542,10.4719349080967,-2.45863363267346));
#6271=CARTESIAN_POINT('Ctrl Pts',(40.2799612282044,10.5102243622422,-2.56333938966843));
#6272=CARTESIAN_POINT('Ctrl Pts',(40.3883369165899,10.5856178404929,-2.70618088325176));
#6273=CARTESIAN_POINT('Ctrl Pts',(40.4362950734393,10.6210495499161,-2.75984467984969));
#6274=CARTESIAN_POINT('Ctrl Pts',(40.4874595913632,10.6607311620303,-2.80916081150993));
#6275=CARTESIAN_POINT('',(44.4440437425414,10.9462182239883,-1.31258522269331));
#6276=CARTESIAN_POINT('',(65.0333054217745,10.9462182239883,-1.3125852226933));
#6277=CARTESIAN_POINT('',(44.4440437425414,10.6607311620303,-2.80916081150993));
#6278=CARTESIAN_POINT('Ctrl Pts',(44.4440437425414,10.6607311620303,-2.80916081150993));
#6279=CARTESIAN_POINT('Ctrl Pts',(44.494558600482,10.6212040619198,-2.76003670668311));
#6280=CARTESIAN_POINT('Ctrl Pts',(44.5419028922086,10.5859075119841,-2.70661428432213));
#6281=CARTESIAN_POINT('Ctrl Pts',(44.6493790253187,10.5104289226276,-2.5638995056778));
#6282=CARTESIAN_POINT('Ctrl Pts',(44.7111607127654,10.4720241652918,-2.45900666288089));
#6283=CARTESIAN_POINT('Ctrl Pts',(44.7971423090715,10.4344613310455,-2.23194048388096));
#6284=CARTESIAN_POINT('Ctrl Pts',(44.8208830494268,10.4356768042938,-2.10953192894979));
#6285=CARTESIAN_POINT('Ctrl Pts',(44.8208830494268,10.4794174046805,-1.88023567177453));
#6286=CARTESIAN_POINT('Ctrl Pts',(44.7971423090715,10.5233488807639,-1.76597563018215));
#6287=CARTESIAN_POINT('Ctrl Pts',(44.7111607127654,10.6418625563635,-1.56868263776198));
#6288=CARTESIAN_POINT('Ctrl Pts',(44.6493790253187,10.7161840275151,-1.48529347310667));
#6289=CARTESIAN_POINT('Ctrl Pts',(44.5419028922086,10.8388990591367,-1.38038614967855));
#6290=CARTESIAN_POINT('Ctrl Pts',(44.494558600482,10.8913830666349,-1.34370876420452));
#6291=CARTESIAN_POINT('Ctrl Pts',(44.4440437425414,10.9462182239883,-1.3125852226933));
#6292=CARTESIAN_POINT('',(65.0333054217745,10.6607311620303,-2.80916081150994));
#6293=CARTESIAN_POINT('Origin',(65.0333054217745,10.5377236573627,-4.95867635844021));
#6294=CARTESIAN_POINT('',(40.4874595913632,10.2758959788686,-3.99356171925254));
#6295=CARTESIAN_POINT('',(40.4874595913632,9.62719480361945,-5.37212188871111));
#6296=CARTESIAN_POINT('Ctrl Pts',(40.4874595913632,10.2758959788686,-3.99356171925253));
#6297=CARTESIAN_POINT('Ctrl Pts',(40.4362950734394,10.214805585414,-4.0101350414746));
#6298=CARTESIAN_POINT('Ctrl Pts',(40.3883369165899,10.1545979421286,-4.03272372864254));
#6299=CARTESIAN_POINT('Ctrl Pts',(40.2799612282044,10.009643213615,-4.10396974981855));
#6300=CARTESIAN_POINT('Ctrl Pts',(40.2177890646542,9.9171218947142,-4.16617251017131));
#6301=CARTESIAN_POINT('Ctrl Pts',(40.1312057824654,9.75351267814105,-4.32762790339198));
#6302=CARTESIAN_POINT('Ctrl Pts',(40.107260046221,9.68258883427222,-4.42729570408678));
#6303=CARTESIAN_POINT('Ctrl Pts',(40.107260046221,9.58320437552114,-4.63849842966349));
#6304=CARTESIAN_POINT('Ctrl Pts',(40.1312057824654,9.55161757473464,-4.75667683776135));
#6305=CARTESIAN_POINT('Ctrl Pts',(40.2177890646542,9.53150249572827,-4.9856554466843));
#6306=CARTESIAN_POINT('Ctrl Pts',(40.2799612282044,9.54254975336982,-5.09659387981389));
#6307=CARTESIAN_POINT('Ctrl Pts',(40.3883369165899,9.58005137194069,-5.25369734080832));
#6308=CARTESIAN_POINT('Ctrl Pts',(40.4362950734393,9.60102428553722,-5.31448669837381));
#6309=CARTESIAN_POINT('Ctrl Pts',(40.4874595913632,9.62719480361944,-5.37212188871111));
#6310=CARTESIAN_POINT('',(44.4440437425414,10.2758959788686,-3.99356171925254));
#6311=CARTESIAN_POINT('',(65.0333054217745,10.2758959788686,-3.99356171925253));
#6312=CARTESIAN_POINT('',(44.4440437425414,9.62719480361945,-5.37212188871111));
#6313=CARTESIAN_POINT('Ctrl Pts',(44.4440437425414,9.62719480361944,-5.37212188871111));
#6314=CARTESIAN_POINT('Ctrl Pts',(44.494558600482,9.6011261881307,-5.31471111790392));
#6315=CARTESIAN_POINT('Ctrl Pts',(44.5419028922086,9.58022416040606,-5.25418916415755));
#6316=CARTESIAN_POINT('Ctrl Pts',(44.6493790253187,9.54260859192743,-5.09718727084803));
#6317=CARTESIAN_POINT('Ctrl Pts',(44.7111607127654,9.53149617990425,-4.98603895482358));
#6318=CARTESIAN_POINT('Ctrl Pts',(44.7971423090715,9.55158251360353,-4.75676498037213));
#6319=CARTESIAN_POINT('Ctrl Pts',(44.8208830494268,9.58320157023845,-4.63850439119268));
#6320=CARTESIAN_POINT('Ctrl Pts',(44.8208830494268,9.68259163955492,-4.42728974255759));
#6321=CARTESIAN_POINT('Ctrl Pts',(44.7971423090715,9.75355824438383,-4.32754470411152));
#6322=CARTESIAN_POINT('Ctrl Pts',(44.7111607127654,9.91741336695648,-4.16592318645703));
#6323=CARTESIAN_POINT('Ctrl Pts',(44.6493790253187,10.0101379343731,-4.10363684402592));
#6324=CARTESIAN_POINT('Ctrl Pts',(44.5419028922086,10.1550870380453,-4.03254336444178));
#6325=CARTESIAN_POINT('Ctrl Pts',(44.494558600482,10.2150434587916,-4.01007050838009));
#6326=CARTESIAN_POINT('Ctrl Pts',(44.4440437425414,10.2758959788686,-3.99356171925253));
#6327=CARTESIAN_POINT('',(65.0333054217745,9.62719480361944,-5.37212188871111));
#6328=CARTESIAN_POINT('Origin',(65.0333054217745,8.9734890270808,-7.42351572959578));
#6329=CARTESIAN_POINT('',(40.4874595913632,8.9599013972947,-6.42360804569852));
#6330=CARTESIAN_POINT('',(40.4874595913632,7.98874638935144,-7.59753279036232));
#6331=CARTESIAN_POINT('Ctrl Pts',(40.4874595913632,8.9599013972947,-6.42360804569851));
#6332=CARTESIAN_POINT('Ctrl Pts',(40.4362950734394,8.89660865325455,-6.42446812347171));
#6333=CARTESIAN_POINT('Ctrl Pts',(40.3883369165899,8.83267496573407,-6.43137411347946));
#6334=CARTESIAN_POINT('Ctrl Pts',(40.2799612282044,8.67455609160262,-6.46433303480991));
#6335=CARTESIAN_POINT('Ctrl Pts',(40.2177890646542,8.56947230261642,-6.50157246470552));
#6336=CARTESIAN_POINT('Ctrl Pts',(40.1312057824654,8.370850846916,-6.61726748224375));
#6337=CARTESIAN_POINT('Ctrl Pts',(40.107260046221,8.27736883191338,-6.69616599297443));
#6338=CARTESIAN_POINT('Ctrl Pts',(40.107260046221,8.12858273669663,-6.87601748671975));
#6339=CARTESIAN_POINT('Ctrl Pts',(40.1312057824654,8.06859851836572,-6.98262778488883));
#6340=CARTESIAN_POINT('Ctrl Pts',(40.2177890646542,7.99217072713916,-7.19941019302185));
#6341=CARTESIAN_POINT('Ctrl Pts',(40.2799612282044,7.97528164845017,-7.30961063252953));
#6342=CARTESIAN_POINT('Ctrl Pts',(40.3883369165899,7.97253504272508,-7.47110467269465));
#6343=CARTESIAN_POINT('Ctrl Pts',(40.4362950734393,7.97773135520069,-7.53519997232425));
#6344=CARTESIAN_POINT('Ctrl Pts',(40.4874595913632,7.98874638935144,-7.59753279036232));
#6345=CARTESIAN_POINT('',(44.4440437425414,8.9599013972947,-6.42360804569852));
#6346=CARTESIAN_POINT('',(65.0333054217745,8.95990139729471,-6.42360804569851));
#6347=CARTESIAN_POINT('',(44.4440437425414,7.98874638935144,-7.59753279036232));
#6348=CARTESIAN_POINT('Ctrl Pts',(44.4440437425414,7.98874638935144,-7.59753279036232));
#6349=CARTESIAN_POINT('Ctrl Pts',(44.494558600482,7.97777424546919,-7.53544268344662));
#6350=CARTESIAN_POINT('Ctrl Pts',(44.5419028922086,7.97258009122984,-7.47162401525292));
#6351=CARTESIAN_POINT('Ctrl Pts',(44.6493790253187,7.97519106813697,-7.31020001364741));
#6352=CARTESIAN_POINT('Ctrl Pts',(44.7111607127654,7.99206923514248,-7.19978008186615));
#6353=CARTESIAN_POINT('Ctrl Pts',(44.7971423090715,8.06854263856859,-6.98270443898868));
#6354=CARTESIAN_POINT('Ctrl Pts',(44.8208830494268,8.12857853697502,-6.87602256331111));
#6355=CARTESIAN_POINT('Ctrl Pts',(44.8208830494268,8.27737303163499,-6.69616091638308));
#6356=CARTESIAN_POINT('Ctrl Pts',(44.7971423090715,8.37091567243115,-6.61719822868546));
#6357=CARTESIAN_POINT('Ctrl Pts',(44.7111607127654,8.5698166220086,-6.50140346015324));
#6358=CARTESIAN_POINT('Ctrl Pts',(44.6493790253187,8.67511806010238,-6.46413361991442));
#6359=CARTESIAN_POINT('Ctrl Pts',(44.5419028922086,8.83319355055587,-6.43132104896007));
#6360=CARTESIAN_POINT('Ctrl Pts',(44.494558600482,8.89685510213054,-6.42446477450645));
#6361=CARTESIAN_POINT('Ctrl Pts',(44.4440437425414,8.9599013972947,-6.42360804569851));
#6362=CARTESIAN_POINT('',(65.0333054217745,7.98874638935144,-7.59753279036232));
#6363=CARTESIAN_POINT('Origin',(65.0333054217745,6.8454170790433,-9.42190830567978));
#6364=CARTESIAN_POINT('',(40.4874595913632,7.08092325871652,-8.45003545425543));
#6365=CARTESIAN_POINT('',(40.4874595913632,5.84833565888647,-9.34556276502401));
#6366=CARTESIAN_POINT('Ctrl Pts',(40.4874595913632,7.08092325871652,-8.45003545425542));
#6367=CARTESIAN_POINT('Ctrl Pts',(40.4362950734394,7.01940507997324,-8.4351282457301));
#6368=CARTESIAN_POINT('Ctrl Pts',(40.3883369165899,6.95576253693625,-8.42591760982703));
#6369=CARTESIAN_POINT('Ctrl Pts',(40.2799612282044,6.79441470756918,-8.41851850107028));
#6370=CARTESIAN_POINT('Ctrl Pts',(40.2177890646542,6.68337124943072,-8.42845471017137));
#6371=CARTESIAN_POINT('Ctrl Pts',(40.1312057824654,6.46221767114332,-8.49111980857872));
#6372=CARTESIAN_POINT('Ctrl Pts',(40.107260046221,6.35205130381232,-8.54429154574763));
#6373=CARTESIAN_POINT('Ctrl Pts',(40.107260046221,6.16321234968933,-8.68149107686204));
#6374=CARTESIAN_POINT('Ctrl Pts',(40.1312057824654,6.07859974285827,-8.76983454798312));
#6375=CARTESIAN_POINT('Ctrl Pts',(40.2177890646542,5.95066147861605,-8.96079951935329));
#6376=CARTESIAN_POINT('Ctrl Pts',(40.2799612282044,5.90689726652424,-9.06333766633592));
#6377=CARTESIAN_POINT('Ctrl Pts',(40.3883369165899,5.86407501584219,-9.21907502119462));
#6378=CARTESIAN_POINT('Ctrl Pts',(40.4362950734394,5.85316822377335,-9.28244891948659));
#6379=CARTESIAN_POINT('Ctrl Pts',(40.4874595913632,5.84833565888646,-9.34556276502401));
#6380=CARTESIAN_POINT('',(44.4440437425414,7.08092325871652,-8.45003545425543));
#6381=CARTESIAN_POINT('',(65.0333054217745,7.08092325871653,-8.45003545425542));
#6382=CARTESIAN_POINT('',(44.4440437425414,5.84833565888647,-9.34556276502401));
#6383=CARTESIAN_POINT('Ctrl Pts',(44.4440437425414,5.84833565888646,-9.34556276502401));
#6384=CARTESIAN_POINT('Ctrl Pts',(44.494558600482,5.85314940676356,-9.28269467176876));
#6385=CARTESIAN_POINT('Ctrl Pts',(44.5419028922086,5.86398949382312,-9.21958925075899));
#6386=CARTESIAN_POINT('Ctrl Pts',(44.6493790253187,5.90666295883444,-9.06388600455431));
#6387=CARTESIAN_POINT('Ctrl Pts',(44.7111607127654,5.95047118756212,-8.96113254742616));
#6388=CARTESIAN_POINT('Ctrl Pts',(44.7971423090715,6.07852655552828,-8.76989489711302));
#6389=CARTESIAN_POINT('Ctrl Pts',(44.8208830494268,6.16320701941278,-8.68149494953464));
#6390=CARTESIAN_POINT('Ctrl Pts',(44.8208830494268,6.35205663408888,-8.54428767307503));
#6391=CARTESIAN_POINT('Ctrl Pts',(44.7971423090715,6.46229768270531,-8.49106885219836));
#6392=CARTESIAN_POINT('Ctrl Pts',(44.7111607127654,6.68374678111908,-8.42837664395866));
#6393=CARTESIAN_POINT('Ctrl Pts',(44.6493790253187,6.79500861326298,-8.41846510704323));
#6394=CARTESIAN_POINT('Ctrl Pts',(44.5419028922086,6.9562780260716,-8.42599517922791));
#6395=CARTESIAN_POINT('Ctrl Pts',(44.494558600482,7.01964461905841,-8.43518629132191));
#6396=CARTESIAN_POINT('Ctrl Pts',(44.4440437425414,7.08092325871652,-8.45003545425542));
#6397=CARTESIAN_POINT('',(65.0333054217745,5.84833565888646,-9.34556276502402));
#6398=CARTESIAN_POINT('Origin',(65.0333054217745,4.28722240024657,-10.8282877315631));
#6399=CARTESIAN_POINT('',(40.4874595913632,4.75702466997909,-9.94551605816494));
#6400=CARTESIAN_POINT('',(40.4874595913632,3.34045249029966,-10.5063766605837));
#6401=CARTESIAN_POINT('Ctrl Pts',(40.4874595913632,4.7570246699791,-9.94551605816493));
#6402=CARTESIAN_POINT('Ctrl Pts',(40.4362950734394,4.70114646995116,-9.91577823807761));
#6403=CARTESIAN_POINT('Ctrl Pts',(40.3883369165899,4.64179396643758,-9.89102971439186));
#6404=CARTESIAN_POINT('Ctrl Pts',(40.2799612282044,4.48735525934981,-9.84373748876312));
#6405=CARTESIAN_POINT('Ctrl Pts',(40.2177890646542,4.37732940092321,-9.82574614850904));
#6406=CARTESIAN_POINT('Ctrl Pts',(40.1312057824654,4.1475395927186,-9.83144384918648));
#6407=CARTESIAN_POINT('Ctrl Pts',(40.107260046221,4.02761103108218,-9.85554783699533));
#6408=CARTESIAN_POINT('Ctrl Pts',(40.107260046221,3.8105846640416,-9.94147465435431));
#6409=CARTESIAN_POINT('Ctrl Pts',(40.1312057824654,3.70666018998099,-10.0060003532323));
#6410=CARTESIAN_POINT('Ctrl Pts',(40.2177890646542,3.53525028438945,-10.1591488563684));
#6411=CARTESIAN_POINT('Ctrl Pts',(40.2799612282044,3.46736080529406,-10.2475818619421));
#6412=CARTESIAN_POINT('Ctrl Pts',(40.3883369165899,3.38715358915463,-10.3877769807267));
#6413=CARTESIAN_POINT('Ctrl Pts',(40.4362950734393,3.3608290063994,-10.4464474625785));
#6414=CARTESIAN_POINT('Ctrl Pts',(40.4874595913632,3.34045249029966,-10.5063766605837));
#6415=CARTESIAN_POINT('',(44.4440437425414,4.75702466997909,-9.94551605816494));
#6416=CARTESIAN_POINT('',(65.0333054217745,4.7570246699791,-9.94551605816493));
#6417=CARTESIAN_POINT('',(44.4440437425414,3.34045249029966,-10.5063766605837));
#6418=CARTESIAN_POINT('Ctrl Pts',(44.4440437425414,3.34045249029966,-10.5063766605837));
#6419=CARTESIAN_POINT('Ctrl Pts',(44.494558600482,3.36074966445325,-10.4466808145007));
#6420=CARTESIAN_POINT('Ctrl Pts',(44.5419028922086,3.38694287027472,-10.3882537863625));
#6421=CARTESIAN_POINT('Ctrl Pts',(44.6493790253187,3.46699749264154,-10.2480547031541));
#6422=CARTESIAN_POINT('Ctrl Pts',(44.7111607127654,3.53498315096504,-10.1594240982912));
#6423=CARTESIAN_POINT('Ctrl Pts',(44.7971423090715,3.70657429374724,-10.0060406054345));
#6424=CARTESIAN_POINT('Ctrl Pts',(44.8208830494268,3.81057853813097,-9.94147707977391));
#6425=CARTESIAN_POINT('Ctrl Pts',(44.8208830494268,4.02761715699281,-9.85554541157574));
#6426=CARTESIAN_POINT('Ctrl Pts',(44.7971423090715,4.14762976290671,-9.83141439176083));
#6427=CARTESIAN_POINT('Ctrl Pts',(44.7111607127654,4.37771254887065,-9.82576392582316));
#6428=CARTESIAN_POINT('Ctrl Pts',(44.6493790253187,4.48794378495868,-9.84383347054759));
#6429=CARTESIAN_POINT('Ctrl Pts',(44.5419028922086,4.64227396980827,-9.89123304374228));
#6430=CARTESIAN_POINT('Ctrl Pts',(44.494558600482,4.7013640481238,-9.91589403100848));
#6431=CARTESIAN_POINT('Ctrl Pts',(44.4440437425414,4.7570246699791,-9.94551605816493));
#6432=CARTESIAN_POINT('',(65.0333054217745,3.34045249029966,-10.5063766605837));
#6433=CARTESIAN_POINT('Origin',(65.0333054217745,1.45964577074129,-11.5542860156157));
#6434=CARTESIAN_POINT('',(40.4874595913632,2.13422472611394,-10.8160833110905));
#6435=CARTESIAN_POINT('',(40.4874595913632,0.622676406422437,-11.0070362708084));
#6436=CARTESIAN_POINT('Ctrl Pts',(40.4874595913632,2.13422472611395,-10.8160833110905));
#6437=CARTESIAN_POINT('Ctrl Pts',(40.4362950734394,2.08749753761475,-10.7733834160453));
#6438=CARTESIAN_POINT('Ctrl Pts',(40.3883369165899,2.03616440970357,-10.7346520453388));
#6439=CARTESIAN_POINT('Ctrl Pts',(40.2799612282044,1.89833877684727,-10.6504382473029));
#6440=CARTESIAN_POINT('Ctrl Pts',(40.2177890646542,1.79624384746427,-10.6056498197694));
#6441=CARTESIAN_POINT('Ctrl Pts',(40.1312057824654,1.57225634809974,-10.5540221152286));
#6442=CARTESIAN_POINT('Ctrl Pts',(40.107260046221,1.45010114475192,-10.5475438114751));
#6443=CARTESIAN_POINT('Ctrl Pts',(40.107260046221,1.21852392960205,-10.5767988171273));
#6444=CARTESIAN_POINT('Ctrl Pts',(40.1312057824654,1.10181754522459,-10.6134523567928));
#6445=CARTESIAN_POINT('Ctrl Pts',(40.2177890646542,0.897706313053607,-10.719161508002));
#6446=CARTESIAN_POINT('Ctrl Pts',(40.2799612282044,0.809957312606231,-10.7879328011928));
#6447=CARTESIAN_POINT('Ctrl Pts',(40.3883369165899,0.697404845380977,-10.9037767089884));
#6448=CARTESIAN_POINT('Ctrl Pts',(40.4362950734394,0.657316542288901,-10.9540572922503));
#6449=CARTESIAN_POINT('Ctrl Pts',(40.4874595913632,0.622676406422431,-11.0070362708084));
#6450=CARTESIAN_POINT('',(44.4440437425414,2.13422472611394,-10.8160833110905));
#6451=CARTESIAN_POINT('',(65.0333054217745,2.13422472611395,-10.8160833110905));
#6452=CARTESIAN_POINT('',(44.4440437425414,0.622676406422437,-11.0070362708084));
#6453=CARTESIAN_POINT('Ctrl Pts',(44.4440437425414,0.622676406422432,-11.0070362708084));
#6454=CARTESIAN_POINT('Ctrl Pts',(44.494558600482,0.657181660752668,-10.9542635814532));
#6455=CARTESIAN_POINT('Ctrl Pts',(44.5419028922086,0.697082169882407,-10.9041861312438));
#6456=CARTESIAN_POINT('Ctrl Pts',(44.6493790253187,0.809487823261111,-10.788300435046));
#6457=CARTESIAN_POINT('Ctrl Pts',(44.7111607127654,0.897379122234209,-10.7193616693125));
#6458=CARTESIAN_POINT('Ctrl Pts',(44.7971423090715,1.10172433726337,-10.6134699828733));
#6459=CARTESIAN_POINT('Ctrl Pts',(44.8208830494268,1.21851739297085,-10.5767996428959));
#6460=CARTESIAN_POINT('Ctrl Pts',(44.8208830494268,1.45010768138313,-10.5475429857066));
#6461=CARTESIAN_POINT('Ctrl Pts',(44.7971423090715,1.57235101118944,-10.5540160076761));
#6462=CARTESIAN_POINT('Ctrl Pts',(44.7111607127654,1.79661053707614,-10.6057623235963));
#6463=CARTESIAN_POINT('Ctrl Pts',(44.6493790253187,1.89888494314277,-10.6506775740104));
#6464=CARTESIAN_POINT('Ctrl Pts',(44.5419028922086,2.0365787669325,-10.7349683587078));
#6465=CARTESIAN_POINT('Ctrl Pts',(44.494558600482,2.08767948363808,-10.7735496806195));
#6466=CARTESIAN_POINT('Ctrl Pts',(44.4440437425414,2.13422472611394,-10.8160833110905));
#6467=CARTESIAN_POINT('',(65.0333054217745,0.622676406422429,-11.0070362708084));
#6468=CARTESIAN_POINT('Origin',(65.0333054217745,-1.45964577074129,-11.5542860156157));
#6469=CARTESIAN_POINT('',(40.4874595913632,-0.622676406422435,-11.0070362708084));
#6470=CARTESIAN_POINT('',(40.4874595913632,-2.13422472611394,-10.8160833110905));
#6471=CARTESIAN_POINT('Ctrl Pts',(40.4874595913632,-0.62267640642243,-11.0070362708084));
#6472=CARTESIAN_POINT('Ctrl Pts',(40.4362950734394,-0.657316542288899,-10.9540572922503));
#6473=CARTESIAN_POINT('Ctrl Pts',(40.3883369165899,-0.697404845380975,-10.9037767089884));
#6474=CARTESIAN_POINT('Ctrl Pts',(40.2799612282044,-0.809957312606229,-10.7879328011928));
#6475=CARTESIAN_POINT('Ctrl Pts',(40.2177890646542,-0.897706313053603,-10.719161508002));
#6476=CARTESIAN_POINT('Ctrl Pts',(40.1312057824654,-1.10181754522459,-10.6134523567928));
#6477=CARTESIAN_POINT('Ctrl Pts',(40.107260046221,-1.21852392960205,-10.5767988171273));
#6478=CARTESIAN_POINT('Ctrl Pts',(40.107260046221,-1.45010114475192,-10.5475438114751));
#6479=CARTESIAN_POINT('Ctrl Pts',(40.1312057824654,-1.57225634809973,-10.5540221152286));
#6480=CARTESIAN_POINT('Ctrl Pts',(40.2177890646542,-1.79624384746427,-10.6056498197694));
#6481=CARTESIAN_POINT('Ctrl Pts',(40.2799612282044,-1.89833877684727,-10.6504382473029));
#6482=CARTESIAN_POINT('Ctrl Pts',(40.3883369165899,-2.03616440970357,-10.7346520453388));
#6483=CARTESIAN_POINT('Ctrl Pts',(40.4362950734394,-2.08749753761475,-10.7733834160453));
#6484=CARTESIAN_POINT('Ctrl Pts',(40.4874595913632,-2.13422472611394,-10.8160833110905));
#6485=CARTESIAN_POINT('',(44.4440437425414,-0.622676406422435,-11.0070362708084));
#6486=CARTESIAN_POINT('',(65.0333054217745,-0.622676406422428,-11.0070362708084));
#6487=CARTESIAN_POINT('',(44.4440437425414,-2.13422472611394,-10.8160833110905));
#6488=CARTESIAN_POINT('Ctrl Pts',(44.4440437425414,-2.13422472611394,-10.8160833110905));
#6489=CARTESIAN_POINT('Ctrl Pts',(44.494558600482,-2.08767948363808,-10.7735496806195));
#6490=CARTESIAN_POINT('Ctrl Pts',(44.5419028922086,-2.0365787669325,-10.7349683587078));
#6491=CARTESIAN_POINT('Ctrl Pts',(44.6493790253187,-1.89888494314277,-10.6506775740104));
#6492=CARTESIAN_POINT('Ctrl Pts',(44.7111607127654,-1.79661053707614,-10.6057623235963));
#6493=CARTESIAN_POINT('Ctrl Pts',(44.7971423090715,-1.57235101118944,-10.5540160076761));
#6494=CARTESIAN_POINT('Ctrl Pts',(44.8208830494268,-1.45010768138313,-10.5475429857066));
#6495=CARTESIAN_POINT('Ctrl Pts',(44.8208830494268,-1.21851739297084,-10.5767996428959));
#6496=CARTESIAN_POINT('Ctrl Pts',(44.7971423090715,-1.10172433726336,-10.6134699828733));
#6497=CARTESIAN_POINT('Ctrl Pts',(44.7111607127654,-0.897379122234208,-10.7193616693125));
#6498=CARTESIAN_POINT('Ctrl Pts',(44.6493790253187,-0.80948782326111,-10.788300435046));
#6499=CARTESIAN_POINT('Ctrl Pts',(44.5419028922086,-0.697082169882405,-10.9041861312438));
#6500=CARTESIAN_POINT('Ctrl Pts',(44.494558600482,-0.657181660752664,-10.9542635814532));
#6501=CARTESIAN_POINT('Ctrl Pts',(44.4440437425414,-0.62267640642243,-11.0070362708084));
#6502=CARTESIAN_POINT('',(65.0333054217745,-2.13422472611394,-10.8160833110905));
#6503=CARTESIAN_POINT('Origin',(65.0333054217745,-4.28722240024656,-10.8282877315631));
#6504=CARTESIAN_POINT('',(40.4874595913632,-3.34045249029966,-10.5063766605837));
#6505=CARTESIAN_POINT('',(40.4874595913632,-4.75702466997909,-9.94551605816494));
#6506=CARTESIAN_POINT('Ctrl Pts',(40.4874595913632,-3.34045249029965,-10.5063766605837));
#6507=CARTESIAN_POINT('Ctrl Pts',(40.4362950734394,-3.3608290063994,-10.4464474625785));
#6508=CARTESIAN_POINT('Ctrl Pts',(40.3883369165899,-3.38715358915463,-10.3877769807267));
#6509=CARTESIAN_POINT('Ctrl Pts',(40.2799612282044,-3.46736080529405,-10.2475818619421));
#6510=CARTESIAN_POINT('Ctrl Pts',(40.2177890646542,-3.53525028438945,-10.1591488563684));
#6511=CARTESIAN_POINT('Ctrl Pts',(40.1312057824654,-3.70666018998098,-10.0060003532323));
#6512=CARTESIAN_POINT('Ctrl Pts',(40.107260046221,-3.8105846640416,-9.94147465435432));
#6513=CARTESIAN_POINT('Ctrl Pts',(40.107260046221,-4.02761103108217,-9.85554783699534));
#6514=CARTESIAN_POINT('Ctrl Pts',(40.1312057824654,-4.14753959271859,-9.83144384918648));
#6515=CARTESIAN_POINT('Ctrl Pts',(40.2177890646542,-4.3773294009232,-9.82574614850904));
#6516=CARTESIAN_POINT('Ctrl Pts',(40.2799612282044,-4.4873552593498,-9.84373748876312));
#6517=CARTESIAN_POINT('Ctrl Pts',(40.3883369165899,-4.64179396643757,-9.89102971439187));
#6518=CARTESIAN_POINT('Ctrl Pts',(40.4362950734394,-4.70114646995115,-9.91577823807761));
#6519=CARTESIAN_POINT('Ctrl Pts',(40.4874595913632,-4.75702466997909,-9.94551605816493));
#6520=CARTESIAN_POINT('',(44.4440437425414,-3.34045249029966,-10.5063766605837));
#6521=CARTESIAN_POINT('',(65.0333054217745,-3.34045249029965,-10.5063766605837));
#6522=CARTESIAN_POINT('',(44.4440437425414,-4.75702466997909,-9.94551605816494));
#6523=CARTESIAN_POINT('Ctrl Pts',(44.4440437425414,-4.75702466997909,-9.94551605816493));
#6524=CARTESIAN_POINT('Ctrl Pts',(44.494558600482,-4.70136404812379,-9.91589403100848));
#6525=CARTESIAN_POINT('Ctrl Pts',(44.5419028922086,-4.64227396980827,-9.89123304374228));
#6526=CARTESIAN_POINT('Ctrl Pts',(44.6493790253187,-4.48794378495868,-9.84383347054759));
#6527=CARTESIAN_POINT('Ctrl Pts',(44.7111607127654,-4.37771254887065,-9.82576392582317));
#6528=CARTESIAN_POINT('Ctrl Pts',(44.7971423090715,-4.14762976290671,-9.83141439176083));
#6529=CARTESIAN_POINT('Ctrl Pts',(44.8208830494268,-4.02761715699281,-9.85554541157574));
#6530=CARTESIAN_POINT('Ctrl Pts',(44.8208830494268,-3.81057853813097,-9.94147707977391));
#6531=CARTESIAN_POINT('Ctrl Pts',(44.7971423090715,-3.70657429374724,-10.0060406054345));
#6532=CARTESIAN_POINT('Ctrl Pts',(44.7111607127654,-3.53498315096503,-10.1594240982912));
#6533=CARTESIAN_POINT('Ctrl Pts',(44.6493790253187,-3.46699749264153,-10.2480547031541));
#6534=CARTESIAN_POINT('Ctrl Pts',(44.5419028922086,-3.38694287027471,-10.3882537863625));
#6535=CARTESIAN_POINT('Ctrl Pts',(44.494558600482,-3.36074966445324,-10.4466808145008));
#6536=CARTESIAN_POINT('Ctrl Pts',(44.4440437425414,-3.34045249029965,-10.5063766605837));
#6537=CARTESIAN_POINT('',(65.0333054217745,-4.7570246699791,-9.94551605816494));
#6538=CARTESIAN_POINT('Origin',(65.0333054217745,-6.8454170790433,-9.42190830567978));
#6539=CARTESIAN_POINT('',(40.4874595913632,-5.84833565888647,-9.34556276502401));
#6540=CARTESIAN_POINT('',(40.4874595913632,-7.08092325871652,-8.45003545425543));
#6541=CARTESIAN_POINT('Ctrl Pts',(40.4874595913632,-5.84833565888646,-9.34556276502402));
#6542=CARTESIAN_POINT('Ctrl Pts',(40.4362950734394,-5.85316822377335,-9.28244891948659));
#6543=CARTESIAN_POINT('Ctrl Pts',(40.3883369165899,-5.86407501584219,-9.21907502119462));
#6544=CARTESIAN_POINT('Ctrl Pts',(40.2799612282044,-5.90689726652424,-9.06333766633591));
#6545=CARTESIAN_POINT('Ctrl Pts',(40.2177890646542,-5.95066147861605,-8.96079951935328));
#6546=CARTESIAN_POINT('Ctrl Pts',(40.1312057824654,-6.07859974285827,-8.76983454798312));
#6547=CARTESIAN_POINT('Ctrl Pts',(40.107260046221,-6.16321234968933,-8.68149107686204));
#6548=CARTESIAN_POINT('Ctrl Pts',(40.107260046221,-6.35205130381232,-8.54429154574763));
#6549=CARTESIAN_POINT('Ctrl Pts',(40.1312057824654,-6.46221767114332,-8.49111980857872));
#6550=CARTESIAN_POINT('Ctrl Pts',(40.2177890646542,-6.68337124943071,-8.42845471017137));
#6551=CARTESIAN_POINT('Ctrl Pts',(40.2799612282044,-6.79441470756917,-8.41851850107028));
#6552=CARTESIAN_POINT('Ctrl Pts',(40.3883369165899,-6.95576253693625,-8.42591760982703));
#6553=CARTESIAN_POINT('Ctrl Pts',(40.4362950734394,-7.01940507997324,-8.4351282457301));
#6554=CARTESIAN_POINT('Ctrl Pts',(40.4874595913632,-7.08092325871652,-8.45003545425542));
#6555=CARTESIAN_POINT('',(44.4440437425414,-5.84833565888647,-9.34556276502401));
#6556=CARTESIAN_POINT('',(65.0333054217745,-5.84833565888646,-9.34556276502402));
#6557=CARTESIAN_POINT('',(44.4440437425414,-7.08092325871652,-8.45003545425543));
#6558=CARTESIAN_POINT('Ctrl Pts',(44.4440437425414,-7.08092325871652,-8.45003545425542));
#6559=CARTESIAN_POINT('Ctrl Pts',(44.494558600482,-7.0196446190584,-8.43518629132191));
#6560=CARTESIAN_POINT('Ctrl Pts',(44.5419028922086,-6.9562780260716,-8.42599517922791));
#6561=CARTESIAN_POINT('Ctrl Pts',(44.6493790253187,-6.79500861326297,-8.41846510704323));
#6562=CARTESIAN_POINT('Ctrl Pts',(44.7111607127654,-6.68374678111907,-8.42837664395866));
#6563=CARTESIAN_POINT('Ctrl Pts',(44.7971423090715,-6.4622976827053,-8.49106885219836));
#6564=CARTESIAN_POINT('Ctrl Pts',(44.8208830494268,-6.35205663408888,-8.54428767307503));
#6565=CARTESIAN_POINT('Ctrl Pts',(44.8208830494268,-6.16320701941278,-8.68149494953464));
#6566=CARTESIAN_POINT('Ctrl Pts',(44.7971423090715,-6.07852655552829,-8.76989489711301));
#6567=CARTESIAN_POINT('Ctrl Pts',(44.7111607127654,-5.95047118756212,-8.96113254742615));
#6568=CARTESIAN_POINT('Ctrl Pts',(44.6493790253187,-5.90666295883444,-9.06388600455431));
#6569=CARTESIAN_POINT('Ctrl Pts',(44.5419028922086,-5.86398949382312,-9.21958925075898));
#6570=CARTESIAN_POINT('Ctrl Pts',(44.494558600482,-5.85314940676355,-9.28269467176876));
#6571=CARTESIAN_POINT('Ctrl Pts',(44.4440437425414,-5.84833565888646,-9.34556276502402));
#6572=CARTESIAN_POINT('',(65.0333054217745,-7.08092325871653,-8.45003545425542));
#6573=CARTESIAN_POINT('Origin',(65.0333054217745,-8.97348902708079,-7.42351572959578));
#6574=CARTESIAN_POINT('',(40.4874595913632,-7.98874638935144,-7.59753279036232));
#6575=CARTESIAN_POINT('',(40.4874595913632,-8.9599013972947,-6.42360804569852));
#6576=CARTESIAN_POINT('Ctrl Pts',(40.4874595913632,-7.98874638935143,-7.59753279036232));
#6577=CARTESIAN_POINT('Ctrl Pts',(40.4362950734394,-7.97773135520069,-7.53519997232426));
#6578=CARTESIAN_POINT('Ctrl Pts',(40.3883369165899,-7.97253504272507,-7.47110467269465));
#6579=CARTESIAN_POINT('Ctrl Pts',(40.2799612282044,-7.97528164845017,-7.30961063252953));
#6580=CARTESIAN_POINT('Ctrl Pts',(40.2177890646542,-7.99217072713915,-7.19941019302185));
#6581=CARTESIAN_POINT('Ctrl Pts',(40.1312057824654,-8.06859851836571,-6.98262778488883));
#6582=CARTESIAN_POINT('Ctrl Pts',(40.107260046221,-8.12858273669663,-6.87601748671976));
#6583=CARTESIAN_POINT('Ctrl Pts',(40.107260046221,-8.27736883191338,-6.69616599297443));
#6584=CARTESIAN_POINT('Ctrl Pts',(40.1312057824654,-8.370850846916,-6.61726748224376));
#6585=CARTESIAN_POINT('Ctrl Pts',(40.2177890646542,-8.56947230261641,-6.50157246470553));
#6586=CARTESIAN_POINT('Ctrl Pts',(40.2799612282044,-8.67455609160262,-6.46433303480991));
#6587=CARTESIAN_POINT('Ctrl Pts',(40.3883369165899,-8.83267496573407,-6.43137411347947));
#6588=CARTESIAN_POINT('Ctrl Pts',(40.4362950734394,-8.89660865325455,-6.42446812347171));
#6589=CARTESIAN_POINT('Ctrl Pts',(40.4874595913632,-8.9599013972947,-6.42360804569852));
#6590=CARTESIAN_POINT('',(44.4440437425414,-7.98874638935144,-7.59753279036232));
#6591=CARTESIAN_POINT('',(65.0333054217745,-7.98874638935143,-7.59753279036232));
#6592=CARTESIAN_POINT('',(44.4440437425414,-8.9599013972947,-6.42360804569852));
#6593=CARTESIAN_POINT('Ctrl Pts',(44.4440437425414,-8.9599013972947,-6.42360804569852));
#6594=CARTESIAN_POINT('Ctrl Pts',(44.494558600482,-8.89685510213054,-6.42446477450646));
#6595=CARTESIAN_POINT('Ctrl Pts',(44.5419028922086,-8.83319355055587,-6.43132104896007));
#6596=CARTESIAN_POINT('Ctrl Pts',(44.6493790253187,-8.67511806010238,-6.46413361991443));
#6597=CARTESIAN_POINT('Ctrl Pts',(44.7111607127654,-8.5698166220086,-6.50140346015324));
#6598=CARTESIAN_POINT('Ctrl Pts',(44.7971423090715,-8.37091567243115,-6.61719822868546));
#6599=CARTESIAN_POINT('Ctrl Pts',(44.8208830494268,-8.27737303163499,-6.69616091638308));
#6600=CARTESIAN_POINT('Ctrl Pts',(44.8208830494268,-8.12857853697502,-6.87602256331111));
#6601=CARTESIAN_POINT('Ctrl Pts',(44.7971423090715,-8.06854263856858,-6.98270443898868));
#6602=CARTESIAN_POINT('Ctrl Pts',(44.7111607127654,-7.99206923514248,-7.19978008186616));
#6603=CARTESIAN_POINT('Ctrl Pts',(44.6493790253187,-7.97519106813697,-7.31020001364741));
#6604=CARTESIAN_POINT('Ctrl Pts',(44.5419028922086,-7.97258009122984,-7.47162401525293));
#6605=CARTESIAN_POINT('Ctrl Pts',(44.494558600482,-7.97777424546919,-7.53544268344662));
#6606=CARTESIAN_POINT('Ctrl Pts',(44.4440437425414,-7.98874638935143,-7.59753279036232));
#6607=CARTESIAN_POINT('',(65.0333054217745,-8.9599013972947,-6.42360804569852));
#6608=CARTESIAN_POINT('Origin',(65.0333054217745,-10.5377236573627,-4.95867635844022));
#6609=CARTESIAN_POINT('',(40.4874595913632,-9.62719480361945,-5.37212188871111));
#6610=CARTESIAN_POINT('',(40.4874595913632,-10.2758959788686,-3.99356171925254));
#6611=CARTESIAN_POINT('Ctrl Pts',(40.4874595913632,-9.62719480361944,-5.37212188871112));
#6612=CARTESIAN_POINT('Ctrl Pts',(40.4362950734394,-9.60102428553722,-5.31448669837382));
#6613=CARTESIAN_POINT('Ctrl Pts',(40.3883369165899,-9.58005137194069,-5.25369734080832));
#6614=CARTESIAN_POINT('Ctrl Pts',(40.2799612282044,-9.54254975336982,-5.0965938798139));
#6615=CARTESIAN_POINT('Ctrl Pts',(40.2177890646542,-9.53150249572826,-4.9856554466843));
#6616=CARTESIAN_POINT('Ctrl Pts',(40.1312057824654,-9.55161757473464,-4.75667683776135));
#6617=CARTESIAN_POINT('Ctrl Pts',(40.107260046221,-9.58320437552114,-4.6384984296635));
#6618=CARTESIAN_POINT('Ctrl Pts',(40.107260046221,-9.68258883427221,-4.42729570408679));
#6619=CARTESIAN_POINT('Ctrl Pts',(40.1312057824654,-9.75351267814104,-4.32762790339198));
#6620=CARTESIAN_POINT('Ctrl Pts',(40.2177890646542,-9.9171218947142,-4.16617251017132));
#6621=CARTESIAN_POINT('Ctrl Pts',(40.2799612282044,-10.009643213615,-4.10396974981856));
#6622=CARTESIAN_POINT('Ctrl Pts',(40.3883369165899,-10.1545979421286,-4.03272372864255));
#6623=CARTESIAN_POINT('Ctrl Pts',(40.4362950734393,-10.214805585414,-4.01013504147461));
#6624=CARTESIAN_POINT('Ctrl Pts',(40.4874595913632,-10.2758959788686,-3.99356171925254));
#6625=CARTESIAN_POINT('',(44.4440437425414,-9.62719480361945,-5.37212188871111));
#6626=CARTESIAN_POINT('',(65.0333054217745,-9.62719480361944,-5.37212188871112));
#6627=CARTESIAN_POINT('',(44.4440437425414,-10.2758959788686,-3.99356171925254));
#6628=CARTESIAN_POINT('Ctrl Pts',(44.4440437425414,-10.2758959788686,-3.99356171925254));
#6629=CARTESIAN_POINT('Ctrl Pts',(44.494558600482,-10.2150434587916,-4.0100705083801));
#6630=CARTESIAN_POINT('Ctrl Pts',(44.5419028922086,-10.1550870380453,-4.03254336444179));
#6631=CARTESIAN_POINT('Ctrl Pts',(44.6493790253187,-10.0101379343731,-4.10363684402592));
#6632=CARTESIAN_POINT('Ctrl Pts',(44.7111607127654,-9.91741336695648,-4.16592318645703));
#6633=CARTESIAN_POINT('Ctrl Pts',(44.7971423090715,-9.75355824438383,-4.32754470411152));
#6634=CARTESIAN_POINT('Ctrl Pts',(44.8208830494268,-9.68259163955491,-4.4272897425576));
#6635=CARTESIAN_POINT('Ctrl Pts',(44.8208830494268,-9.58320157023844,-4.63850439119269));
#6636=CARTESIAN_POINT('Ctrl Pts',(44.7971423090715,-9.55158251360353,-4.75676498037214));
#6637=CARTESIAN_POINT('Ctrl Pts',(44.7111607127654,-9.53149617990424,-4.98603895482358));
#6638=CARTESIAN_POINT('Ctrl Pts',(44.6493790253187,-9.54260859192742,-5.09718727084803));
#6639=CARTESIAN_POINT('Ctrl Pts',(44.5419028922086,-9.58022416040605,-5.25418916415756));
#6640=CARTESIAN_POINT('Ctrl Pts',(44.494558600482,-9.60112618813069,-5.31471111790393));
#6641=CARTESIAN_POINT('Ctrl Pts',(44.4440437425414,-9.62719480361944,-5.37212188871112));
#6642=CARTESIAN_POINT('',(65.0333054217745,-10.2758959788686,-3.99356171925253));
#6643=CARTESIAN_POINT('Origin',(65.0333054217745,-11.4398343552159,-2.18226511494789));
#6644=CARTESIAN_POINT('',(40.4874595913632,-10.6607311620303,-2.80916081150993));
#6645=CARTESIAN_POINT('',(40.4874595913632,-10.9462182239883,-1.31258522269331));
#6646=CARTESIAN_POINT('Ctrl Pts',(40.4874595913632,-10.6607311620303,-2.80916081150993));
#6647=CARTESIAN_POINT('Ctrl Pts',(40.4362950734394,-10.6210495499161,-2.7598446798497));
#6648=CARTESIAN_POINT('Ctrl Pts',(40.3883369165899,-10.5856178404929,-2.70618088325177));
#6649=CARTESIAN_POINT('Ctrl Pts',(40.2799612282044,-10.5102243622422,-2.56333938966843));
#6650=CARTESIAN_POINT('Ctrl Pts',(40.2177890646542,-10.4719349080967,-2.45863363267347));
#6651=CARTESIAN_POINT('Ctrl Pts',(40.1312057824654,-10.4344733704908,-2.23184639108363));
#6652=CARTESIAN_POINT('Ctrl Pts',(40.107260046221,-10.4356780388714,-2.10952545706757));
#6653=CARTESIAN_POINT('Ctrl Pts',(40.107260046221,-10.479416170103,-1.88024214365675));
#6654=CARTESIAN_POINT('Ctrl Pts',(40.1312057824654,-10.5233254368881,-1.76606754746801));
#6655=CARTESIAN_POINT('Ctrl Pts',(40.2177890646542,-10.6416422455441,-1.56899661471236));
#6656=CARTESIAN_POINT('Ctrl Pts',(40.2799612282044,-10.7157876396233,-1.48573895210117));
#6657=CARTESIAN_POINT('Ctrl Pts',(40.3883369165899,-10.8384701838204,-1.38068248061461));
#6658=CARTESIAN_POINT('Ctrl Pts',(40.4362950734394,-10.8911687152148,-1.34383042657664));
#6659=CARTESIAN_POINT('Ctrl Pts',(40.4874595913632,-10.9462182239883,-1.31258522269331));
#6660=CARTESIAN_POINT('',(44.4440437425414,-10.6607311620303,-2.80916081150993));
#6661=CARTESIAN_POINT('',(65.0333054217746,-10.6607311620303,-2.80916081150993));
#6662=CARTESIAN_POINT('',(44.4440437425414,-10.9462182239883,-1.31258522269331));
#6663=CARTESIAN_POINT('Ctrl Pts',(44.4440437425414,-10.9462182239883,-1.31258522269331));
#6664=CARTESIAN_POINT('Ctrl Pts',(44.494558600482,-10.8913830666349,-1.34370876420452));
#6665=CARTESIAN_POINT('Ctrl Pts',(44.5419028922086,-10.8388990591367,-1.38038614967856));
#6666=CARTESIAN_POINT('Ctrl Pts',(44.6493790253187,-10.7161840275151,-1.48529347310667));
#6667=CARTESIAN_POINT('Ctrl Pts',(44.7111607127654,-10.6418625563635,-1.56868263776198));
#6668=CARTESIAN_POINT('Ctrl Pts',(44.7971423090715,-10.5233488807639,-1.76597563018215));
#6669=CARTESIAN_POINT('Ctrl Pts',(44.8208830494268,-10.4794174046805,-1.88023567177453));
#6670=CARTESIAN_POINT('Ctrl Pts',(44.8208830494268,-10.4356768042938,-2.10953192894979));
#6671=CARTESIAN_POINT('Ctrl Pts',(44.7971423090715,-10.4344613310455,-2.23194048388096));
#6672=CARTESIAN_POINT('Ctrl Pts',(44.7111607127654,-10.4720241652918,-2.45900666288089));
#6673=CARTESIAN_POINT('Ctrl Pts',(44.6493790253187,-10.5104289226276,-2.5638995056778));
#6674=CARTESIAN_POINT('Ctrl Pts',(44.5419028922086,-10.5859075119841,-2.70661428432213));
#6675=CARTESIAN_POINT('Ctrl Pts',(44.494558600482,-10.6212040619198,-2.76003670668311));
#6676=CARTESIAN_POINT('Ctrl Pts',(44.4440437425414,-10.6607311620303,-2.80916081150993));
#6677=CARTESIAN_POINT('',(65.0333054217746,-10.9462182239883,-1.31258522269331));
#6678=CARTESIAN_POINT('Origin',(65.0333054217745,-11.6231381877631,0.731265871526303));
#6679=CARTESIAN_POINT('',(40.4874595913632,-11.0244145741041,-0.0696898291507972));
#6680=CARTESIAN_POINT('',(40.4874595913632,-10.9287493207203,1.45086583075851));
#6681=CARTESIAN_POINT('Ctrl Pts',(40.4874595913632,-11.0244145741041,-0.0696898291508038));
#6682=CARTESIAN_POINT('Ctrl Pts',(40.4362950734394,-10.9737152095859,-0.031791470091884));
#6683=CARTESIAN_POINT('Ctrl Pts',(40.3883369165899,-10.9260510089478,0.0113748718365901));
#6684=CARTESIAN_POINT('Ctrl Pts',(40.2799612282044,-10.8175029205336,0.130979141632737));
#6685=CARTESIAN_POINT('Ctrl Pts',(40.2177890646542,-10.7543771371068,0.222873174700234));
#6686=CARTESIAN_POINT('Ctrl Pts',(40.1312057824654,-10.6616928290704,0.433219172502735));
#6687=CARTESIAN_POINT('Ctrl Pts',(40.107260046221,-10.6324396713002,0.551996758287847));
#6688=CARTESIAN_POINT('Ctrl Pts',(40.107260046221,-10.6177832473694,0.784953945706132));
#6689=CARTESIAN_POINT('Ctrl Pts',(40.1312057824654,-10.6319189563517,0.906461327605488));
#6690=CARTESIAN_POINT('Ctrl Pts',(40.2177890646542,-10.6975090768639,1.12676510841489));
#6691=CARTESIAN_POINT('Ctrl Pts',(40.2799612282044,-10.7486197183239,1.22584628814239));
#6692=CARTESIAN_POINT('Ctrl Pts',(40.3883369165899,-10.8413214827577,1.35811212546531));
#6693=CARTESIAN_POINT('Ctrl Pts',(40.4362950734394,-10.8831996597221,1.40691199628575));
#6694=CARTESIAN_POINT('Ctrl Pts',(40.4874595913632,-10.9287493207203,1.45086583075852));
#6695=CARTESIAN_POINT('',(44.4440437425414,-11.0244145741041,-0.0696898291507972));
#6696=CARTESIAN_POINT('',(65.0333054217745,-11.0244145741041,-0.0696898291508069));
#6697=CARTESIAN_POINT('',(44.4440437425414,-10.9287493207203,1.45086583075851));
#6698=CARTESIAN_POINT('Ctrl Pts',(44.4440437425414,-10.9287493207203,1.45086583075852));
#6699=CARTESIAN_POINT('Ctrl Pts',(44.494558600482,-10.8833770206965,1.40708314344117));
#6700=CARTESIAN_POINT('Ctrl Pts',(44.5419028922086,-10.8416631896602,1.35850580357412));
#6701=CARTESIAN_POINT('Ctrl Pts',(44.6493790253187,-10.7488928668403,1.22637634925516));
#6702=CARTESIAN_POINT('Ctrl Pts',(44.7111607127654,-10.6976443833215,1.12712401027483));
#6703=CARTESIAN_POINT('Ctrl Pts',(44.7971423090715,-10.6319188047956,0.906556187395612));
#6704=CARTESIAN_POINT('Ctrl Pts',(44.8208830494268,-10.6177828336688,0.78496052128923));
#6705=CARTESIAN_POINT('Ctrl Pts',(44.8208830494268,-10.6324400850008,0.551990182704752));
#6706=CARTESIAN_POINT('Ctrl Pts',(44.7971423090715,-10.6617045677936,0.433125041715377));
#6707=CARTESIAN_POINT('Ctrl Pts',(44.7111607127654,-10.7545563589632,0.222534061284506));
#6708=CARTESIAN_POINT('Ctrl Pts',(44.6493790253187,-10.8178403494655,0.130487494796954));
#6709=CARTESIAN_POINT('Ctrl Pts',(44.5419028922086,-10.9264393623398,0.0110271252282851));
#6710=CARTESIAN_POINT('Ctrl Pts',(44.494558600482,-10.9739126224425,-0.0319390384764412));
#6711=CARTESIAN_POINT('Ctrl Pts',(44.4440437425414,-11.0244145741041,-0.0696898291508038));
#6712=CARTESIAN_POINT('',(65.0333054217745,-10.9287493207203,1.45086583075852));
#6713=CARTESIAN_POINT('Origin',(65.0333054217745,-11.0761175010611,3.59884873388475));
#6714=CARTESIAN_POINT('',(40.4874595913632,-10.6953934735264,2.67416002147514));
#6715=CARTESIAN_POINT('',(40.4874595913632,-10.2245869045029,4.1231536481525));
#6716=CARTESIAN_POINT('Ctrl Pts',(40.4874595913632,-10.6953934735264,2.67416002147514));
#6717=CARTESIAN_POINT('Ctrl Pts',(40.4362950734394,-10.636861984136,2.69825931465265));
#6718=CARTESIAN_POINT('Ctrl Pts',(40.3883369165899,-10.5799602093058,2.7282159018936));
#6719=CARTESIAN_POINT('Ctrl Pts',(40.2799612282044,-10.445077986335,2.81706777175753));
#6720=CARTESIAN_POINT('Ctrl Pts',(40.2177890646542,-10.3610822987601,2.89037604083732));
#6721=CARTESIAN_POINT('Ctrl Pts',(40.1312057824654,-10.2189989162361,3.07106398221209));
#6722=CARTESIAN_POINT('Ctrl Pts',(40.107260046221,-10.1611260158034,3.17883498721797));
#6723=CARTESIAN_POINT('Ctrl Pts',(40.107260046221,-10.0889959537284,3.40082849180162));
#6724=CARTESIAN_POINT('Ctrl Pts',(40.1312057824654,-10.072469906325,3.52203390373397));
#6725=CARTESIAN_POINT('Ctrl Pts',(40.2177890646542,-10.0812120701981,3.75172803582824));
#6726=CARTESIAN_POINT('Ctrl Pts',(40.2799612282044,-10.1060764894642,3.86040709775467));
#6727=CARTESIAN_POINT('Ctrl Pts',(40.3883369165899,-10.162972681342,4.01157155191524));
#6728=CARTESIAN_POINT('Ctrl Pts',(40.4362950734394,-10.1913991440005,4.06925296416112));
#6729=CARTESIAN_POINT('Ctrl Pts',(40.4874595913632,-10.2245869045029,4.12315364815251));
#6730=CARTESIAN_POINT('',(44.4440437425414,-10.6953934735264,2.67416002147514));
#6731=CARTESIAN_POINT('',(65.0333054217745,-10.6953934735264,2.67416002147513));
#6732=CARTESIAN_POINT('',(44.4440437425414,-10.2245869045029,4.1231536481525));
#6733=CARTESIAN_POINT('Ctrl Pts',(44.4440437425414,-10.2245869045029,4.12315364815251));
#6734=CARTESIAN_POINT('Ctrl Pts',(44.494558600482,-10.191528370287,4.06946284229464));
#6735=CARTESIAN_POINT('Ctrl Pts',(44.5419028922086,-10.1632057491294,4.01203784095338));
#6736=CARTESIAN_POINT('Ctrl Pts',(44.6493790253187,-10.1062092356792,3.86098843529658));
#6737=CARTESIAN_POINT('Ctrl Pts',(44.7111607127654,-10.0812538704914,3.75210931147394));
#6738=CARTESIAN_POINT('Ctrl Pts',(44.7971423090715,-10.0724461688598,3.52212574563888));
#6739=CARTESIAN_POINT('Ctrl Pts',(44.8208830494268,-10.088993917744,3.40083475791753));
#6740=CARTESIAN_POINT('Ctrl Pts',(44.8208830494268,-10.1611280517879,3.17882872110207));
#6741=CARTESIAN_POINT('Ctrl Pts',(44.7971423090715,-10.2190336955406,3.07097572801825));
#6742=CARTESIAN_POINT('Ctrl Pts',(44.7111607127654,-10.3613402241094,2.89009215195637));
#6743=CARTESIAN_POINT('Ctrl Pts',(44.6493790253187,-10.4455270819127,2.81667548607418));
#6744=CARTESIAN_POINT('Ctrl Pts',(44.5419028922086,-10.5804228429266,2.72797565994568));
#6745=CARTESIAN_POINT('Ctrl Pts',(44.494558600482,-10.6370898936696,2.69816547698127));
#6746=CARTESIAN_POINT('Ctrl Pts',(44.4440437425414,-10.6953934735264,2.67416002147514));
#6747=CARTESIAN_POINT('',(65.0333054217745,-10.2245869045029,4.12315364815251));
#6748=CARTESIAN_POINT('Origin',(65.0333054217745,-9.83314361665672,6.24030269465341));
#6749=CARTESIAN_POINT('',(40.4874595913632,-9.69434146610128,5.2499825630792));
#6750=CARTESIAN_POINT('',(40.4874595913632,-8.87797608967546,6.53636855793469));
#6751=CARTESIAN_POINT('Ctrl Pts',(40.4874595913632,-9.69434146610128,5.24998256307919));
#6752=CARTESIAN_POINT('Ctrl Pts',(40.4362950734394,-9.63165560058094,5.25876854315396));
#6753=CARTESIAN_POINT('Ctrl Pts',(40.3883369165899,-9.56909159934126,5.27363309315841));
#6754=CARTESIAN_POINT('Ctrl Pts',(40.2799612282044,-9.4163503879453,5.32614967333225));
#6755=CARTESIAN_POINT('Ctrl Pts',(40.2177890646542,-9.31676255418716,5.3762659502691));
#6756=CARTESIAN_POINT('Ctrl Pts',(40.1312057824654,-9.13420771864564,5.51594254733579));
#6757=CARTESIAN_POINT('Ctrl Pts',(40.107260046221,-9.05135144272633,5.6059353229639));
#6758=CARTESIAN_POINT('Ctrl Pts',(40.107260046221,-8.92627993958308,5.80301647638493));
#6759=CARTESIAN_POINT('Ctrl Pts',(40.1312057824654,-8.88013052813091,5.91630413655623));
#6760=CARTESIAN_POINT('Ctrl Pts',(40.2177890646542,-8.83147543305722,6.14095609285995));
#6761=CARTESIAN_POINT('Ctrl Pts',(40.2799612282044,-8.82853130722192,6.25240433183085));
#6762=CARTESIAN_POINT('Ctrl Pts',(40.3883369165899,-8.8460469295586,6.41296918423019));
#6763=CARTESIAN_POINT('Ctrl Pts',(40.4362950734394,-8.85923553871714,6.4759078026327));
#6764=CARTESIAN_POINT('Ctrl Pts',(40.4874595913632,-8.87797608967545,6.53636855793469));
#6765=CARTESIAN_POINT('',(44.4440437425414,-9.69434146610128,5.2499825630792));
#6766=CARTESIAN_POINT('',(65.0333054217745,-9.69434146610129,5.24998256307919));
#6767=CARTESIAN_POINT('',(44.4440437425414,-8.87797608967546,6.53636855793469));
#6768=CARTESIAN_POINT('Ctrl Pts',(44.4440437425414,-8.87797608967545,6.53636855793469));
#6769=CARTESIAN_POINT('Ctrl Pts',(44.494558600482,-8.85930851055284,6.47614322432933));
#6770=CARTESIAN_POINT('Ctrl Pts',(44.5419028922086,-8.8461567137246,6.4134787855425));
#6771=CARTESIAN_POINT('Ctrl Pts',(44.6493790253187,-8.82851531020285,6.25300041822613));
#6772=CARTESIAN_POINT('Ctrl Pts',(44.7111607127654,-8.83142110072016,6.14133578534036));
#6773=CARTESIAN_POINT('Ctrl Pts',(44.7971423090715,-8.88008469626887,5.91638718981127));
#6774=CARTESIAN_POINT('Ctrl Pts',(44.8208830494268,-8.92627640924315,5.80302203931053));
#6775=CARTESIAN_POINT('Ctrl Pts',(44.8208830494268,-9.05135497306626,5.6059297600383));
#6776=CARTESIAN_POINT('Ctrl Pts',(44.7971423090715,-9.13426335321985,5.51586571507106));
#6777=CARTESIAN_POINT('Ctrl Pts',(44.7111607127654,-9.31708297663107,5.37605512370539));
#6778=CARTESIAN_POINT('Ctrl Pts',(44.6493790253187,-9.41688293184191,5.32588139755355));
#6779=CARTESIAN_POINT('Ctrl Pts',(44.5419028922086,-9.56959944421904,5.27351545115601));
#6780=CARTESIAN_POINT('Ctrl Pts',(44.494558600482,-9.6318996863973,5.25873433236176));
#6781=CARTESIAN_POINT('Ctrl Pts',(44.4440437425414,-9.69434146610128,5.24998256307919));
#6782=CARTESIAN_POINT('',(65.0333054217745,-8.87797608967545,6.5363685579347));
#6783=CARTESIAN_POINT('Origin',(65.0333054217745,-7.97231715504529,8.48965548688909));
#6784=CARTESIAN_POINT('',(40.4874595913632,-8.08415833106712,7.49592939215974));
#6785=CARTESIAN_POINT('',(40.4874595913632,-6.97352938622158,8.53887939213984));
#6786=CARTESIAN_POINT('Ctrl Pts',(40.4874595913632,-8.08415833106713,7.49592939215973));
#6787=CARTESIAN_POINT('Ctrl Pts',(40.4362950734394,-8.02125687288993,7.48885000369108));
#6788=CARTESIAN_POINT('Ctrl Pts',(40.3883369165899,-7.95696177153298,7.48768852211428));
#6789=CARTESIAN_POINT('Ctrl Pts',(40.2799612282044,-7.79595886376674,7.50057000272323));
#6790=CARTESIAN_POINT('Ctrl Pts',(40.2177890646542,-7.68703635367879,7.52434529752241));
#6791=CARTESIAN_POINT('Ctrl Pts',(40.1312057824654,-7.47548065682658,7.61423415599275));
#6792=CARTESIAN_POINT('Ctrl Pts',(40.107260046221,-7.3728471699607,7.68079412518008));
#6793=CARTESIAN_POINT('Ctrl Pts',(40.107260046221,-7.20269292827251,7.84057959375527));
#6794=CARTESIAN_POINT('Ctrl Pts',(40.1312057824654,-7.12981989001877,7.93883122183408));
#6795=CARTESIAN_POINT('Ctrl Pts',(40.2177890646542,-7.02682471456273,8.14432529372061));
#6796=CARTESIAN_POINT('Ctrl Pts',(40.2799612282044,-6.99625703388003,8.25154000700348));
#6797=CARTESIAN_POINT('Ctrl Pts',(40.3883369165899,-6.97329151570619,8.41141637744911));
#6798=CARTESIAN_POINT('Ctrl Pts',(40.4362950734394,-6.97041358254702,8.47565753714199));
#6799=CARTESIAN_POINT('Ctrl Pts',(40.4874595913632,-6.97352938622157,8.53887939213984));
#6800=CARTESIAN_POINT('',(44.4440437425414,-8.08415833106712,7.49592939215974));
#6801=CARTESIAN_POINT('',(65.0333054217745,-8.08415833106713,7.49592939215973));
#6802=CARTESIAN_POINT('',(44.4440437425414,-6.97352938622158,8.53887939213984));
#6803=CARTESIAN_POINT('Ctrl Pts',(44.4440437425414,-6.97352938622157,8.53887939213984));
#6804=CARTESIAN_POINT('Ctrl Pts',(44.494558600482,-6.97042571484315,8.47590370999069));
#6805=CARTESIAN_POINT('Ctrl Pts',(44.5419028922086,-6.97327111810788,8.41193727091097));
#6806=CARTESIAN_POINT('Ctrl Pts',(44.6493790253187,-6.99609329877835,8.25211338795166));
#6807=CARTESIAN_POINT('Ctrl Pts',(44.7111607127654,-7.02667766349585,8.14467954556077));
#6808=CARTESIAN_POINT('Ctrl Pts',(44.7971423090715,-7.12975484354433,7.9389002678978));
#6809=CARTESIAN_POINT('Ctrl Pts',(44.8208830494268,-7.20268812540135,7.84058410395149));
#6810=CARTESIAN_POINT('Ctrl Pts',(44.8208830494268,-7.37285197283185,7.68078961498386));
#6811=CARTESIAN_POINT('Ctrl Pts',(44.7971423090715,-7.47555365094558,7.61417357331087));
#6812=CARTESIAN_POINT('Ctrl Pts',(44.7111607127654,-7.68739913989675,7.5242207802843));
#6813=CARTESIAN_POINT('Ctrl Pts',(44.6493790253187,-7.79654139429069,7.500442593603));
#6814=CARTESIAN_POINT('Ctrl Pts',(44.5419028922086,-7.95748291790636,7.48770087193706));
#6815=CARTESIAN_POINT('Ctrl Pts',(44.494558600482,-8.02150179817958,7.48887756936796));
#6816=CARTESIAN_POINT('Ctrl Pts',(44.4440437425414,-8.08415833106713,7.49592939215973));
#6817=CARTESIAN_POINT('',(65.0333054217745,-6.97352938622157,8.53887939213985));
#6818=CARTESIAN_POINT('Origin',(65.0333054217745,-5.61056068645084,10.2055720021147));
#6819=CARTESIAN_POINT('',(40.4874595913632,-5.96601779663743,9.270879409431));
#6820=CARTESIAN_POINT('',(40.4874595913632,-4.63091018458434,10.0048610303352));
#6821=CARTESIAN_POINT('Ctrl Pts',(40.4874595913632,-5.96601779663743,9.270879409431));
#6822=CARTESIAN_POINT('Ctrl Pts',(40.4362950734394,-5.90685307575603,9.24837947643258));
#6823=CARTESIAN_POINT('Ctrl Pts',(40.3883369165899,-5.84486677196091,9.23126494343361));
#6824=CARTESIAN_POINT('Ctrl Pts',(40.2799612282044,-5.68571857264663,9.20370193367626));
#6825=CARTESIAN_POINT('Ctrl Pts',(40.2177890646542,-5.57430538812665,9.19964235712612));
#6826=CARTESIAN_POINT('Ctrl Pts',(40.1312057824654,-5.3470416524444,9.2340954294343));
#6827=CARTESIAN_POINT('Ctrl Pts',(40.107260046221,-5.2310797940713,9.27304038452639));
#6828=CARTESIAN_POINT('Ctrl Pts',(40.107260046221,-5.02653423062696,9.3854902596153));
#6829=CARTESIAN_POINT('Ctrl Pts',(40.1312057824654,-4.93151644657342,9.46253234446524));
#6830=CARTESIAN_POINT('Ctrl Pts',(40.2177890646542,-4.78065275639871,9.63595658364359));
#6831=CARTESIAN_POINT('Ctrl Pts',(40.2799612282044,-4.72438220066596,9.73220107649475));
#6832=CARTESIAN_POINT('Ctrl Pts',(40.3883369165899,-4.66237854994973,9.88134334464741));
#6833=CARTESIAN_POINT('Ctrl Pts',(40.4362950734394,-4.64361490559755,9.94285053730468));
#6834=CARTESIAN_POINT('Ctrl Pts',(40.4874595913632,-4.63091018458433,10.0048610303352));
#6835=CARTESIAN_POINT('',(44.4440437425414,-5.96601779663743,9.270879409431));
#6836=CARTESIAN_POINT('',(65.0333054217745,-5.96601779663744,9.270879409431));
#6837=CARTESIAN_POINT('',(44.4440437425414,-4.63091018458434,10.0048610303352));
#6838=CARTESIAN_POINT('Ctrl Pts',(44.4440437425414,-4.63091018458433,10.0048610303352));
#6839=CARTESIAN_POINT('Ctrl Pts',(44.494558600482,-4.64356543603732,9.94309199336002));
#6840=CARTESIAN_POINT('Ctrl Pts',(44.5419028922086,-4.66222925224323,9.88184280060688));
#6841=CARTESIAN_POINT('Ctrl Pts',(44.6493790253187,-4.72408101556028,9.7327157243621));
#6842=CARTESIAN_POINT('Ctrl Pts',(44.7111607127654,-4.78042222636134,9.63626313589754));
#6843=CARTESIAN_POINT('Ctrl Pts',(44.7971423090715,-4.93143627259579,9.4625830449195));
#6844=CARTESIAN_POINT('Ctrl Pts',(44.8208830494268,-5.02652845700664,9.38549343368993));
#6845=CARTESIAN_POINT('Ctrl Pts',(44.8208830494268,-5.23108556769161,9.27303721045176));
#6846=CARTESIAN_POINT('Ctrl Pts',(44.7971423090715,-5.34712741961925,9.23405490296801));
#6847=CARTESIAN_POINT('Ctrl Pts',(44.7111607127654,-5.57468774292635,9.19961197308963));
#6848=CARTESIAN_POINT('Ctrl Pts',(44.6493790253187,-5.6863144872627,9.20372339679809));
#6849=CARTESIAN_POINT('Ctrl Pts',(44.5419028922086,-5.84536847428662,9.2314065090968));
#6850=CARTESIAN_POINT('Ctrl Pts',(44.494558600482,-5.90708345096224,9.24846708652567));
#6851=CARTESIAN_POINT('Ctrl Pts',(44.4440437425414,-5.96601779663743,9.270879409431));
#6852=CARTESIAN_POINT('',(65.0333054217745,-4.63091018458433,10.0048610303352));
#6853=CARTESIAN_POINT('Origin',(65.0333054217745,-2.89627205572787,11.2802348949791));
#6854=CARTESIAN_POINT('',(40.4874595913632,-3.47301042256638,10.4633059774983));
#6855=CARTESIAN_POINT('',(40.4874595913632,-1.99731386475336,10.8422004546895));
#6856=CARTESIAN_POINT('Ctrl Pts',(40.4874595913632,-3.47301042256639,10.4633059774983));
#6857=CARTESIAN_POINT('Ctrl Pts',(40.4362950734394,-3.42129997598637,10.4267992535094));
#6858=CARTESIAN_POINT('Ctrl Pts',(40.3883369165899,-3.36551729719021,10.3948070381394));
#6859=CARTESIAN_POINT('Ctrl Pts',(40.2799612282044,-3.21822367299693,10.3285314232885));
#6860=CARTESIAN_POINT('Ctrl Pts',(40.2177890646542,-3.11132031417736,10.2968920535137));
#6861=CARTESIAN_POINT('Ctrl Pts',(40.1312057824654,-2.88262835599554,10.2737445264171));
#6862=CARTESIAN_POINT('Ctrl Pts',(40.107260046221,-2.76062443615468,10.282627412656));
#6863=CARTESIAN_POINT('Ctrl Pts',(40.107260046221,-2.53453990097136,10.3406760550451));
#6864=CARTESIAN_POINT('Ctrl Pts',(40.1312057824654,-2.42334768794107,10.391667759134));
#6865=CARTESIAN_POINT('Ctrl Pts',(40.2177890646542,-2.23409480353921,10.5221252828469));
#6866=CARTESIAN_POINT('Ctrl Pts',(40.2799612282044,-2.15565705872172,10.601352159818));
#6867=CARTESIAN_POINT('Ctrl Pts',(40.3883369165899,-2.05851119287108,10.7303891684628));
#6868=CARTESIAN_POINT('Ctrl Pts',(40.4362950734394,-2.02504082610839,10.7852976709622));
#6869=CARTESIAN_POINT('Ctrl Pts',(40.4874595913632,-1.99731386475336,10.8422004546895));
#6870=CARTESIAN_POINT('',(44.4440437425414,-3.47301042256638,10.4633059774983));
#6871=CARTESIAN_POINT('',(65.0333054217745,-3.47301042256639,10.4633059774983));
#6872=CARTESIAN_POINT('',(44.4440437425414,-1.99731386475336,10.8422004546895));
#6873=CARTESIAN_POINT('Ctrl Pts',(44.4440437425414,-1.99731386475336,10.8422004546895));
#6874=CARTESIAN_POINT('Ctrl Pts',(44.494558600482,-2.0249328630462,10.7855192386522));
#6875=CARTESIAN_POINT('Ctrl Pts',(44.5419028922086,-2.05824237598036,10.7308358042651));
#6876=CARTESIAN_POINT('Ctrl Pts',(44.6493790253187,-2.15523734817991,10.6017757373863));
#6877=CARTESIAN_POINT('Ctrl Pts',(44.7111607127654,-2.23379527958143,10.5223648737091));
#6878=CARTESIAN_POINT('Ctrl Pts',(44.7971423090715,-2.42325742408613,10.3916969282828));
#6879=CARTESIAN_POINT('Ctrl Pts',(44.8208830494268,-2.53453351937968,10.3406776935593));
#6880=CARTESIAN_POINT('Ctrl Pts',(44.8208830494268,-2.76063081774636,10.2826257741417));
#6881=CARTESIAN_POINT('Ctrl Pts',(44.7971423090715,-2.8827215071592,10.2737266025933));
#6882=CARTESIAN_POINT('Ctrl Pts',(44.7111607127654,-3.11169821280053,10.2969577118196));
#6883=CARTESIAN_POINT('Ctrl Pts',(44.6493790253187,-3.21879552819819,10.3287004100455));
#6884=CARTESIAN_POINT('Ctrl Pts',(44.5419028922086,-3.36596803166599,10.3950689245517));
#6885=CARTESIAN_POINT('Ctrl Pts',(44.494558600482,-3.42150132578769,10.4269414031543));
#6886=CARTESIAN_POINT('Ctrl Pts',(44.4440437425414,-3.47301042256638,10.4633059774983));
#6887=CARTESIAN_POINT('',(65.0333054217745,-1.99731386475336,10.8422004546896));
#6888=CARTESIAN_POINT('Origin',(45.2000998321956,0.,0.));
#6889=CARTESIAN_POINT('',(45.9561559218497,-1.16412425803185E-15,9.50579594738959));
#6890=CARTESIAN_POINT('Origin',(45.9561559218497,0.,0.));
#6891=CARTESIAN_POINT('',(44.8208830494268,-4.43719969509731E-16,10.6461191435901));
#6892=CARTESIAN_POINT('',(45.2000998321956,-1.25712631749648E-15,10.265215394118));
#6893=CARTESIAN_POINT('',(44.4440437425414,-0.761781030806626,10.9982845496518));
#6894=CARTESIAN_POINT('Ctrl Pts',(44.8208830494268,4.5102810375397E-16,
10.6461191435901));
#6895=CARTESIAN_POINT('Ctrl Pts',(44.8208830494268,-0.11671548063215,10.6461191435901));
#6896=CARTESIAN_POINT('Ctrl Pts',(44.7971423090715,-0.237183600496259,10.6678622756543));
#6897=CARTESIAN_POINT('Ctrl Pts',(44.7111607127654,-0.45318923993895,10.7473077279545));
#6898=CARTESIAN_POINT('Ctrl Pts',(44.6493790253187,-0.549027808195105,10.8046871902268));
#6899=CARTESIAN_POINT('Ctrl Pts',(44.5419028922086,-0.675071438451299,10.9055709290878));
#6900=CARTESIAN_POINT('Ctrl Pts',(44.494558600482,-0.720933688912239,10.9502526438148));
#6901=CARTESIAN_POINT('Ctrl Pts',(44.4440437425414,-0.761781030806632,10.9982845496518));
#6902=CARTESIAN_POINT('Origin',(44.4440437425414,0.,0.));
#6903=CARTESIAN_POINT('Origin',(44.4440437425414,0.,0.));
#6904=CARTESIAN_POINT('Origin',(44.4440437425414,0.,0.));
#6905=CARTESIAN_POINT('Origin',(44.4440437425414,0.,0.));
#6906=CARTESIAN_POINT('Origin',(44.4440437425414,0.,0.));
#6907=CARTESIAN_POINT('Origin',(44.4440437425414,0.,0.));
#6908=CARTESIAN_POINT('Origin',(44.4440437425414,0.,0.));
#6909=CARTESIAN_POINT('Origin',(44.4440437425414,0.,0.));
#6910=CARTESIAN_POINT('Origin',(44.4440437425414,0.,0.));
#6911=CARTESIAN_POINT('Origin',(44.4440437425414,0.,0.));
#6912=CARTESIAN_POINT('Origin',(44.4440437425414,0.,0.));
#6913=CARTESIAN_POINT('Origin',(44.4440437425414,0.,0.));
#6914=CARTESIAN_POINT('Origin',(44.4440437425414,0.,0.));
#6915=CARTESIAN_POINT('Origin',(44.4440437425414,0.,0.));
#6916=CARTESIAN_POINT('Origin',(44.4440437425414,0.,0.));
#6917=CARTESIAN_POINT('Origin',(44.4440437425414,0.,0.));
#6918=CARTESIAN_POINT('Origin',(44.4440437425414,0.,0.));
#6919=CARTESIAN_POINT('Origin',(44.4440437425414,0.,0.));
#6920=CARTESIAN_POINT('Origin',(44.4440437425414,0.,0.));
#6921=CARTESIAN_POINT('Origin',(44.4440437425414,0.,0.));
#6922=CARTESIAN_POINT('Origin',(44.4440437425414,0.,0.));
#6923=CARTESIAN_POINT('Origin',(44.4440437425414,0.,0.));
#6924=CARTESIAN_POINT('Origin',(44.4440437425414,0.,0.));
#6925=CARTESIAN_POINT('Origin',(44.4440437425414,0.,0.));
#6926=CARTESIAN_POINT('',(44.4440437425414,0.761781030806626,10.9982845496518));
#6927=CARTESIAN_POINT('Origin',(44.4440437425414,0.,0.));
#6928=CARTESIAN_POINT('Ctrl Pts',(44.4440437425414,0.761781030806632,10.9982845496518));
#6929=CARTESIAN_POINT('Ctrl Pts',(44.494558600482,0.720933688912238,10.9502526438148));
#6930=CARTESIAN_POINT('Ctrl Pts',(44.5419028922086,0.6750714384513,10.9055709290878));
#6931=CARTESIAN_POINT('Ctrl Pts',(44.6493790253187,0.549027808195106,10.8046871902268));
#6932=CARTESIAN_POINT('Ctrl Pts',(44.7111607127654,0.45318923993895,10.7473077279545));
#6933=CARTESIAN_POINT('Ctrl Pts',(44.7971423090715,0.23718360049626,10.6678622756543));
#6934=CARTESIAN_POINT('Ctrl Pts',(44.8208830494268,0.116715480632151,10.6461191435901));
#6935=CARTESIAN_POINT('Ctrl Pts',(44.8208830494268,3.46944695195361E-17,
10.6461191435901));
#6936=CARTESIAN_POINT('Origin',(42.4657516669523,0.,0.));
#6937=CARTESIAN_POINT('',(40.4874595913632,0.761781030806626,10.9982845496518));
#6938=CARTESIAN_POINT('Origin',(40.4874595913632,0.,0.));
#6939=CARTESIAN_POINT('',(65.0333054217745,0.761781030806634,10.9982845496518));
#6940=CARTESIAN_POINT('Origin',(42.4657516669523,0.,0.));
#6941=CARTESIAN_POINT('',(40.4874595913632,-0.761781030806626,10.9982845496518));
#6942=CARTESIAN_POINT('',(65.0333054217745,-0.761781030806634,10.9982845496518));
#6943=CARTESIAN_POINT('Origin',(40.4874595913632,0.,0.));
#6944=CARTESIAN_POINT('Origin',(42.4657516669523,0.,0.));
#6945=CARTESIAN_POINT('Origin',(40.4874595913632,0.,0.));
#6946=CARTESIAN_POINT('Origin',(42.4657516669523,0.,0.));
#6947=CARTESIAN_POINT('Origin',(40.4874595913632,0.,0.));
#6948=CARTESIAN_POINT('Origin',(42.4657516669523,0.,0.));
#6949=CARTESIAN_POINT('Origin',(40.4874595913632,0.,0.));
#6950=CARTESIAN_POINT('Origin',(42.4657516669523,0.,0.));
#6951=CARTESIAN_POINT('Origin',(40.4874595913632,0.,0.));
#6952=CARTESIAN_POINT('Origin',(42.4657516669523,0.,0.));
#6953=CARTESIAN_POINT('Origin',(40.4874595913632,0.,0.));
#6954=CARTESIAN_POINT('Origin',(42.4657516669523,0.,0.));
#6955=CARTESIAN_POINT('Origin',(40.4874595913632,0.,0.));
#6956=CARTESIAN_POINT('Origin',(42.4657516669523,0.,0.));
#6957=CARTESIAN_POINT('Origin',(40.4874595913632,0.,0.));
#6958=CARTESIAN_POINT('Origin',(42.4657516669523,0.,0.));
#6959=CARTESIAN_POINT('Origin',(40.4874595913632,0.,0.));
#6960=CARTESIAN_POINT('Origin',(42.4657516669523,0.,0.));
#6961=CARTESIAN_POINT('Origin',(40.4874595913632,0.,0.));
#6962=CARTESIAN_POINT('Origin',(42.4657516669523,0.,0.));
#6963=CARTESIAN_POINT('Origin',(40.4874595913632,0.,0.));
#6964=CARTESIAN_POINT('Origin',(42.4657516669523,0.,0.));
#6965=CARTESIAN_POINT('Origin',(40.4874595913632,0.,0.));
#6966=CARTESIAN_POINT('Origin',(42.4657516669523,0.,0.));
#6967=CARTESIAN_POINT('Origin',(40.4874595913632,0.,0.));
#6968=CARTESIAN_POINT('Origin',(42.4657516669523,0.,0.));
#6969=CARTESIAN_POINT('Origin',(40.4874595913632,0.,0.));
#6970=CARTESIAN_POINT('Origin',(42.4657516669523,0.,0.));
#6971=CARTESIAN_POINT('Origin',(40.4874595913632,0.,0.));
#6972=CARTESIAN_POINT('Origin',(42.4657516669523,0.,0.));
#6973=CARTESIAN_POINT('Origin',(40.4874595913632,0.,0.));
#6974=CARTESIAN_POINT('Origin',(42.4657516669523,0.,0.));
#6975=CARTESIAN_POINT('Origin',(40.4874595913632,0.,0.));
#6976=CARTESIAN_POINT('Origin',(42.4657516669523,0.,0.));
#6977=CARTESIAN_POINT('Origin',(40.4874595913632,0.,0.));
#6978=CARTESIAN_POINT('Origin',(42.4657516669523,0.,0.));
#6979=CARTESIAN_POINT('Origin',(40.4874595913632,0.,0.));
#6980=CARTESIAN_POINT('Origin',(42.4657516669523,0.,0.));
#6981=CARTESIAN_POINT('Origin',(40.4874595913632,0.,0.));
#6982=CARTESIAN_POINT('Origin',(42.4657516669523,0.,0.));
#6983=CARTESIAN_POINT('Origin',(40.4874595913632,0.,0.));
#6984=CARTESIAN_POINT('Origin',(42.4657516669523,0.,0.));
#6985=CARTESIAN_POINT('Origin',(40.4874595913632,0.,0.));
#6986=CARTESIAN_POINT('Origin',(42.4657516669523,0.,0.));
#6987=CARTESIAN_POINT('Origin',(40.4874595913632,0.,0.));
#6988=CARTESIAN_POINT('Origin',(65.0333054217745,0.,11.6461191435901));
#6989=CARTESIAN_POINT('',(40.107260046221,-7.55970195185556E-16,10.6461191435901));
#6990=CARTESIAN_POINT('Ctrl Pts',(40.4874595913632,-0.761781030806633,10.9982845496518));
#6991=CARTESIAN_POINT('Ctrl Pts',(40.4362950734394,-0.720774016064355,10.9500648864029));
#6992=CARTESIAN_POINT('Ctrl Pts',(40.3883369165899,-0.674699993130249,10.9052051772128));
#6993=CARTESIAN_POINT('Ctrl Pts',(40.2799612282044,-0.548515944174103,10.804381297894));
#6994=CARTESIAN_POINT('Ctrl Pts',(40.2177890646542,-0.452839542252609,10.7471501528591));
#6995=CARTESIAN_POINT('Ctrl Pts',(40.1312057824654,-0.237088918373978,10.6678564706158));
#6996=CARTESIAN_POINT('Ctrl Pts',(40.107260046221,-0.116708892047988,10.6461191435901));
#6997=CARTESIAN_POINT('Ctrl Pts',(40.107260046221,-1.56125112837913E-16,
10.6461191435901));
#6998=CARTESIAN_POINT('Ctrl Pts',(40.107260046221,1.73472347597681E-17,
10.6461191435901));
#6999=CARTESIAN_POINT('Ctrl Pts',(40.107260046221,0.116708892047988,10.6461191435901));
#7000=CARTESIAN_POINT('Ctrl Pts',(40.1312057824654,0.237088918373978,10.6678564706158));
#7001=CARTESIAN_POINT('Ctrl Pts',(40.2177890646542,0.452839542252609,10.7471501528591));
#7002=CARTESIAN_POINT('Ctrl Pts',(40.2799612282044,0.548515944174103,10.804381297894));
#7003=CARTESIAN_POINT('Ctrl Pts',(40.3883369165899,0.674699993130249,10.9052051772128));
#7004=CARTESIAN_POINT('Ctrl Pts',(40.4362950734394,0.720774016064356,10.9500648864029));
#7005=CARTESIAN_POINT('Ctrl Pts',(40.4874595913632,0.761781030806633,10.9982845496518));
#7006=CARTESIAN_POINT('Origin',(51.9780076285768,0.,0.));
#7007=CARTESIAN_POINT('',(52.9998593353039,-1.16412425803185E-15,9.50579594738959));
#7008=CARTESIAN_POINT('Origin',(52.9998593353039,0.,0.));
#7009=CARTESIAN_POINT('',(51.9780076285768,-1.16412425803185E-15,9.50579594738959));
#7010=CARTESIAN_POINT('Origin',(52.9998593353039,0.,0.));
#7011=CARTESIAN_POINT('Origin',(21.2197085942866,0.,-9.50579594738959));
#7012=CARTESIAN_POINT('',(21.2197085942866,-1.16412425803185E-15,9.50579594738959));
#7013=CARTESIAN_POINT('Origin',(21.2197085942866,0.,0.));
#7014=CARTESIAN_POINT('Origin',(30.0907863269434,0.,0.));
#7015=CARTESIAN_POINT('',(38.9618640596001,-1.16412425803185E-15,9.50579594738959));
#7016=CARTESIAN_POINT('Origin',(38.9618640596001,0.,0.));
#7017=CARTESIAN_POINT('',(30.0907863269434,-1.16412425803185E-15,9.50579594738959));
#7018=CARTESIAN_POINT('Origin',(39.7246618254816,0.,0.));
#7019=CARTESIAN_POINT('Origin',(40.4874595913632,0.,0.));
#7020=CARTESIAN_POINT('',(39.7246618254816,-1.25712631749648E-15,10.265215394118));
#7021=CARTESIAN_POINT('Origin',(42.4657516669523,0.,0.));
#7296=UNCERTAINTY_MEASURE_WITH_UNIT(LENGTH_MEASURE(0.01),#7316,
'DISTANCE_ACCURACY_VALUE',
'Maximum model space distance between geometric entities at asserted c
onnectivities');
#7303=UNCERTAINTY_MEASURE_WITH_UNIT(LENGTH_MEASURE(0.01),#7316,
'DISTANCE_ACCURACY_VALUE',
'Maximum model space distance between geometric entities at asserted c
onnectivities');
#7308=(
GEOMETRIC_REPRESENTATION_CONTEXT(3)
GLOBAL_UNCERTAINTY_ASSIGNED_CONTEXT((#7296))
GLOBAL_UNIT_ASSIGNED_CONTEXT((#7316,#7318,#7319))
REPRESENTATION_CONTEXT('','3D')
);
#7315=(
GEOMETRIC_REPRESENTATION_CONTEXT(3)
GLOBAL_UNCERTAINTY_ASSIGNED_CONTEXT((#7303))
GLOBAL_UNIT_ASSIGNED_CONTEXT((#7316,#7318,#7319))
REPRESENTATION_CONTEXT('','3D')
);
#7316=(
LENGTH_UNIT()
NAMED_UNIT(*)
SI_UNIT(.MILLI.,.METRE.)
);
#7318=(
NAMED_UNIT(*)
PLANE_ANGLE_UNIT()
SI_UNIT($,.RADIAN.)
);
#7319=(
NAMED_UNIT(*)
SI_UNIT($,.STERADIAN.)
SOLID_ANGLE_UNIT()
);
#7324=SHAPE_DEFINITION_REPRESENTATION(#7335,#7356);
#7335=PRODUCT_DEFINITION_SHAPE('',$,#7368);
#7356=SHAPE_REPRESENTATION('',(#3527),#7308);
#7363=PRODUCT_DEFINITION_CONTEXT('part definition',#7398,'design');
#7368=PRODUCT_DEFINITION('Middle_Ring','Middle_Ring',#7379,#7363);
#7379=PRODUCT_DEFINITION_FORMATION('',$,#7404);
#7398=APPLICATION_CONTEXT(
'Core Data for Automotive Mechanical Design Process');
#7399=PRODUCT_CONTEXT('part definition',#7398,'mechanical');
#7404=PRODUCT('Middle_Ring','Middle_Ring',$,(#7399));
#7425=COLOUR_RGB('Light Blue',0.38,0.62,0.78);
#7426=FILL_AREA_STYLE_COLOUR('',#7425);
#7427=FILL_AREA_STYLE('',(#7426));
#7428=SURFACE_STYLE_FILL_AREA(#7427);
#7429=SURFACE_SIDE_STYLE('',(#7428));
#7430=SURFACE_STYLE_USAGE(.BOTH.,#7429);
#7431=PRESENTATION_STYLE_ASSIGNMENT((#7430));
ENDSEC;
END-ISO-10303-21;
